ISO-10303-21;
HEADER;
FILE_DESCRIPTION((''),'2;1');
FILE_NAME('Hex_Nut.step','2026-10-09T10:33:02-07:00',(''),(''),'','','');
FILE_SCHEMA (('AUTOMOTIVE_DESIGN { 1 0 10303 214 3 1 1 }'));
ENDSEC;
DATA;
#10=MECHANICAL_DESIGN_GEOMETRIC_PRESENTATION_REPRESENTATION('',(#839),#86330);
#736=(
BOUNDED_SURFACE()
B_SPLINE_SURFACE(1,2,((#48177,#48178,#48179,#48180,#48181,#48182,#48183,
#48184,#48185,#48186,#48187,#48188,#48189,#48190,#48191,#48192,#48193,#48194,
#48195,#48196,#48197,#48198,#48199,#48200,#48201,#48202,#48203,#48204,#48205,
#48206,#48207,#48208,#48209,#48210,#48211,#48212,#48213,#48214,#48215,#48216,
#48217,#48218,#48219,#48220,#48221,#48222,#48223,#48224,#48225,#48226,#48227,
#48228,#48229,#48230,#48231,#48232,#48233,#48234,#48235,#48236,#48237,#48238,
#48239,#48240,#48241,#48242,#48243,#48244,#48245,#48246,#48247,#48248,#48249,
#48250,#48251,#48252,#48253,#48254,#48255,#48256,#48257,#48258,#48259,#48260,
#48261),(#48262,#48263,#48264,#48265,#48266,#48267,#48268,#48269,#48270,
#48271,#48272,#48273,#48274,#48275,#48276,#48277,#48278,#48279,#48280,#48281,
#48282,#48283,#48284,#48285,#48286,#48287,#48288,#48289,#48290,#48291,#48292,
#48293,#48294,#48295,#48296,#48297,#48298,#48299,#48300,#48301,#48302,#48303,
#48304,#48305,#48306,#48307,#48308,#48309,#48310,#48311,#48312,#48313,#48314,
#48315,#48316,#48317,#48318,#48319,#48320,#48321,#48322,#48323,#48324,#48325,
#48326,#48327,#48328,#48329,#48330,#48331,#48332,#48333,#48334,#48335,#48336,
#48337,#48338,#48339,#48340,#48341,#48342,#48343,#48344,#48345,#48346)),
 .UNSPECIFIED.,.F.,.F.,.F.)
B_SPLINE_SURFACE_WITH_KNOTS((2,2),(3,2,2,2,2,2,2,2,2,2,2,2,2,2,2,2,2,2,
2,2,2,2,2,2,2,2,2,2,2,2,2,2,2,2,2,2,2,2,2,2,2,2,3),(-0.000109059520856525,
1.00010905952086),(-9.68976095313223E-5,0.0238095238095238,0.0476190476190476,
0.0714285714285714,0.0952380952380952,0.119047619047619,0.142857142857143,
0.166666666666667,0.19047619047619,0.214285714285714,0.238095238095238,
0.261904761904762,0.285714285714286,0.30952380952381,0.333333333333333,
0.357142857142857,0.380952380952381,0.404761904761905,0.428571428571429,
0.452380952380952,0.476190476190476,0.5,0.523809523809524,0.547619047619048,
0.571428571428571,0.595238095238095,0.619047619047619,0.642857142857143,
0.666666666666667,0.69047619047619,0.714285714285714,0.738095238095238,
0.761904761904762,0.785714285714286,0.80952380952381,0.833333333333333,
0.857142857142857,0.880952380952381,0.904761904761905,0.928571428571429,
0.952380952380952,0.976190476190476,1.),.UNSPECIFIED.)
GEOMETRIC_REPRESENTATION_ITEM()
RATIONAL_B_SPLINE_SURFACE(((1.00109491061774,0.865480167423768,1.,0.866025403784439,
1.,0.866025403784439,1.,0.866025403784439,1.,0.866025403784439,1.,0.866025403784439,
1.,0.866025403784439,1.,0.866025403784439,1.,0.866025403784439,1.,0.866025403784439,
1.,0.866025403784439,1.,0.866025403784439,1.,0.866025403784439,1.,0.866025403784439,
1.,0.866025403784439,1.,0.866025403784439,1.,0.866025403784439,1.,0.866025403784439,
1.,0.866025403784439,1.,0.866025403784439,1.,0.866025403784439,1.,0.866025403784439,
1.,0.866025403784439,1.,0.866025403784439,1.,0.866025403784439,1.,0.866025403784439,
1.,0.866025403784439,1.,0.866025403784439,1.,0.866025403784439,1.,0.866025403784439,
1.,0.866025403784439,1.,0.866025403784439,1.,0.866025403784439,1.,0.866025403784439,
1.,0.866025403784439,1.,0.866025403784439,1.,0.866025403784439,1.,0.866025403784439,
1.,0.866025403784439,1.,0.866025403784439,1.,0.866025403784439,1.,0.866025403784439,
1.),(1.00109491061774,0.865480167423768,1.,0.866025403784439,1.,0.866025403784439,
1.,0.866025403784439,1.,0.866025403784439,1.,0.866025403784439,1.,0.866025403784439,
1.,0.866025403784439,1.,0.866025403784439,1.,0.866025403784439,1.,0.866025403784439,
1.,0.866025403784439,1.,0.866025403784439,1.,0.866025403784439,1.,0.866025403784439,
1.,0.866025403784439,1.,0.866025403784439,1.,0.866025403784439,1.,0.866025403784439,
1.,0.866025403784439,1.,0.866025403784439,1.,0.866025403784439,1.,0.866025403784439,
1.,0.866025403784439,1.,0.866025403784439,1.,0.866025403784439,1.,0.866025403784439,
1.,0.866025403784439,1.,0.866025403784439,1.,0.866025403784439,1.,0.866025403784439,
1.,0.866025403784439,1.,0.866025403784439,1.,0.866025403784439,1.,0.866025403784439,
1.,0.866025403784439,1.,0.866025403784439,1.,0.866025403784439,1.,0.866025403784439,
1.,0.866025403784439,1.,0.866025403784439,1.,0.866025403784439,1.)))
REPRESENTATION_ITEM('')
SURFACE()
) ;
#737=(
BOUNDED_SURFACE()
B_SPLINE_SURFACE(1,2,((#48347,#48348,#48349,#48350,#48351,#48352,#48353,
#48354,#48355,#48356,#48357,#48358,#48359,#48360,#48361,#48362,#48363,#48364,
#48365,#48366,#48367,#48368,#48369,#48370,#48371,#48372,#48373,#48374,#48375,
#48376,#48377,#48378,#48379,#48380,#48381,#48382,#48383,#48384,#48385,#48386,
#48387,#48388,#48389,#48390,#48391,#48392,#48393,#48394,#48395,#48396,#48397,
#48398,#48399,#48400,#48401,#48402,#48403,#48404,#48405,#48406,#48407,#48408,
#48409,#48410,#48411,#48412,#48413,#48414,#48415,#48416,#48417,#48418,#48419,
#48420,#48421,#48422,#48423,#48424,#48425,#48426,#48427,#48428,#48429,#48430,
#48431),(#48432,#48433,#48434,#48435,#48436,#48437,#48438,#48439,#48440,
#48441,#48442,#48443,#48444,#48445,#48446,#48447,#48448,#48449,#48450,#48451,
#48452,#48453,#48454,#48455,#48456,#48457,#48458,#48459,#48460,#48461,#48462,
#48463,#48464,#48465,#48466,#48467,#48468,#48469,#48470,#48471,#48472,#48473,
#48474,#48475,#48476,#48477,#48478,#48479,#48480,#48481,#48482,#48483,#48484,
#48485,#48486,#48487,#48488,#48489,#48490,#48491,#48492,#48493,#48494,#48495,
#48496,#48497,#48498,#48499,#48500,#48501,#48502,#48503,#48504,#48505,#48506,
#48507,#48508,#48509,#48510,#48511,#48512,#48513,#48514,#48515,#48516)),
 .UNSPECIFIED.,.F.,.F.,.F.)
B_SPLINE_SURFACE_WITH_KNOTS((2,2),(3,2,2,2,2,2,2,2,2,2,2,2,2,2,2,2,2,2,
2,2,2,2,2,2,2,2,2,2,2,2,2,2,2,2,2,2,2,2,2,2,2,2,3),(-9.75032520683202E-5,
1.),(0.,0.0238095238095238,0.0476190476190476,0.0714285714285714,0.0952380952380952,
0.119047619047619,0.142857142857143,0.166666666666667,0.19047619047619,
0.214285714285714,0.238095238095238,0.261904761904762,0.285714285714286,
0.30952380952381,0.333333333333333,0.357142857142857,0.380952380952381,
0.404761904761905,0.428571428571429,0.452380952380952,0.476190476190476,
0.5,0.523809523809524,0.547619047619048,0.571428571428571,0.595238095238095,
0.619047619047619,0.642857142857143,0.666666666666667,0.69047619047619,
0.714285714285714,0.738095238095238,0.761904761904762,0.785714285714286,
0.80952380952381,0.833333333333333,0.857142857142857,0.880952380952381,
0.904761904761905,0.928571428571429,0.952380952380952,0.976190476190476,
1.),.UNSPECIFIED.)
GEOMETRIC_REPRESENTATION_ITEM()
RATIONAL_B_SPLINE_SURFACE(((1.,0.866025403784439,1.,0.866025403784439,1.,
0.866025403784439,1.,0.866025403784439,1.,0.866025403784439,1.,0.866025403784439,
1.,0.866025403784439,1.,0.866025403784439,1.,0.866025403784439,1.,0.866025403784439,
1.,0.866025403784439,1.,0.866025403784439,1.,0.866025403784439,1.,0.866025403784439,
1.,0.866025403784439,1.,0.866025403784439,1.,0.866025403784439,1.,0.866025403784439,
1.,0.866025403784439,1.,0.866025403784439,1.,0.866025403784439,1.,0.866025403784439,
1.,0.866025403784439,1.,0.866025403784439,1.,0.866025403784439,1.,0.866025403784439,
1.,0.866025403784439,1.,0.866025403784439,1.,0.866025403784439,1.,0.866025403784439,
1.,0.866025403784439,1.,0.866025403784439,1.,0.866025403784439,1.,0.866025403784439,
1.,0.866025403784439,1.,0.866025403784439,1.,0.866025403784439,1.,0.866025403784439,
1.,0.866025403784439,1.,0.866025403784439,1.,0.866025403784439,1.,0.866025403784439,
1.),(1.,0.866025403784439,1.,0.866025403784439,1.,0.866025403784439,1.,
0.866025403784439,1.,0.866025403784439,1.,0.866025403784439,1.,0.866025403784439,
1.,0.866025403784439,1.,0.866025403784439,1.,0.866025403784439,1.,0.866025403784439,
1.,0.866025403784439,1.,0.866025403784439,1.,0.866025403784439,1.,0.866025403784439,
1.,0.866025403784439,1.,0.866025403784439,1.,0.866025403784439,1.,0.866025403784439,
1.,0.866025403784439,1.,0.866025403784439,1.,0.866025403784439,1.,0.866025403784439,
1.,0.866025403784439,1.,0.866025403784439,1.,0.866025403784439,1.,0.866025403784439,
1.,0.866025403784439,1.,0.866025403784439,1.,0.866025403784439,1.,0.866025403784439,
1.,0.866025403784439,1.,0.866025403784439,1.,0.866025403784439,1.,0.866025403784439,
1.,0.866025403784439,1.,0.866025403784439,1.,0.866025403784439,1.,0.866025403784439,
1.,0.866025403784439,1.,0.866025403784439,1.,0.866025403784439,1.)))
REPRESENTATION_ITEM('')
SURFACE()
) ;
#764=(
BOUNDED_CURVE()
B_SPLINE_CURVE(2,(#48160,#48161,#48162),.UNSPECIFIED.,.F.,.F.)
B_SPLINE_CURVE_WITH_KNOTS((3,3),(-1.37310606553565,-1.01047077031707),
 .UNSPECIFIED.)
CURVE()
GEOMETRIC_REPRESENTATION_ITEM()
RATIONAL_B_SPLINE_CURVE((2.09743606996414,2.25967331459556,2.25967331459556))
REPRESENTATION_ITEM('')
) ;
#765=(
BOUNDED_CURVE()
B_SPLINE_CURVE(2,(#48163,#48164,#48165),.UNSPECIFIED.,.F.,.F.)
B_SPLINE_CURVE_WITH_KNOTS((3,3),(1.01047077031706,1.37310606553565),
 .UNSPECIFIED.)
CURVE()
GEOMETRIC_REPRESENTATION_ITEM()
RATIONAL_B_SPLINE_CURVE((2.25967331459555,2.25967331459556,2.09743606996414))
REPRESENTATION_ITEM('')
) ;
#766=(
BOUNDED_CURVE()
B_SPLINE_CURVE(2,(#48171,#48172,#48173),.UNSPECIFIED.,.F.,.F.)
B_SPLINE_CURVE_WITH_KNOTS((3,3),(1.01047077031707,1.37310606553565),
 .UNSPECIFIED.)
CURVE()
GEOMETRIC_REPRESENTATION_ITEM()
RATIONAL_B_SPLINE_CURVE((2.25967331459556,2.25967331459556,2.09743606996414))
REPRESENTATION_ITEM('')
) ;
#767=(
BOUNDED_CURVE()
B_SPLINE_CURVE(2,(#48174,#48175,#48176),.UNSPECIFIED.,.F.,.F.)
B_SPLINE_CURVE_WITH_KNOTS((3,3),(-1.37310606553565,-1.01047077031707),
 .UNSPECIFIED.)
CURVE()
GEOMETRIC_REPRESENTATION_ITEM()
RATIONAL_B_SPLINE_CURVE((2.09743606996414,2.25967331459556,2.25967331459556))
REPRESENTATION_ITEM('')
) ;
#768=(
BOUNDED_CURVE()
B_SPLINE_CURVE(2,(#48532,#48533,#48534),.UNSPECIFIED.,.F.,.F.)
B_SPLINE_CURVE_WITH_KNOTS((3,3),(-1.37310606553565,-1.01047077031706),
 .UNSPECIFIED.)
CURVE()
GEOMETRIC_REPRESENTATION_ITEM()
RATIONAL_B_SPLINE_CURVE((2.09743606996414,2.25967331459555,2.25967331459555))
REPRESENTATION_ITEM('')
) ;
#769=(
BOUNDED_CURVE()
B_SPLINE_CURVE(2,(#48536,#48537,#48538),.UNSPECIFIED.,.F.,.F.)
B_SPLINE_CURVE_WITH_KNOTS((3,3),(-1.01047077031706,-0.647835475111481),
 .UNSPECIFIED.)
CURVE()
GEOMETRIC_REPRESENTATION_ITEM()
RATIONAL_B_SPLINE_CURVE((2.25967331459555,2.25967331459555,2.09743606997577))
REPRESENTATION_ITEM('')
) ;
#770=(
BOUNDED_CURVE()
B_SPLINE_CURVE(2,(#48541,#48542,#48543),.UNSPECIFIED.,.F.,.F.)
B_SPLINE_CURVE_WITH_KNOTS((3,3),(1.01047077031706,1.37310606553561),
 .UNSPECIFIED.)
CURVE()
GEOMETRIC_REPRESENTATION_ITEM()
RATIONAL_B_SPLINE_CURVE((2.25967331459555,2.25967331459555,2.09743606996417))
REPRESENTATION_ITEM('')
) ;
#771=(
BOUNDED_CURVE()
B_SPLINE_CURVE(2,(#48544,#48545,#48546),.UNSPECIFIED.,.F.,.F.)
B_SPLINE_CURVE_WITH_KNOTS((3,3),(0.647835475111436,1.01047077031706),
 .UNSPECIFIED.)
CURVE()
GEOMETRIC_REPRESENTATION_ITEM()
RATIONAL_B_SPLINE_CURVE((2.09743606997573,2.25967331459555,2.25967331459555))
REPRESENTATION_ITEM('')
) ;
#772=(
BOUNDED_CURVE()
B_SPLINE_CURVE(2,(#48549,#48550,#48551),.UNSPECIFIED.,.F.,.F.)
B_SPLINE_CURVE_WITH_KNOTS((3,3),(-1.3731060655357,-1.01047077031707),
 .UNSPECIFIED.)
CURVE()
GEOMETRIC_REPRESENTATION_ITEM()
RATIONAL_B_SPLINE_CURVE((2.09743606996409,2.25967331459555,2.25967331459555))
REPRESENTATION_ITEM('')
) ;
#773=(
BOUNDED_CURVE()
B_SPLINE_CURVE(2,(#48553,#48554,#48555),.UNSPECIFIED.,.F.,.F.)
B_SPLINE_CURVE_WITH_KNOTS((3,3),(-1.01047077031707,-0.647835475111438),
 .UNSPECIFIED.)
CURVE()
GEOMETRIC_REPRESENTATION_ITEM()
RATIONAL_B_SPLINE_CURVE((2.25967331459555,2.25967331459555,2.09743606997573))
REPRESENTATION_ITEM('')
) ;
#774=(
BOUNDED_CURVE()
B_SPLINE_CURVE(2,(#48558,#48559,#48560),.UNSPECIFIED.,.F.,.F.)
B_SPLINE_CURVE_WITH_KNOTS((3,3),(1.01047077031707,1.37310606553565),
 .UNSPECIFIED.)
CURVE()
GEOMETRIC_REPRESENTATION_ITEM()
RATIONAL_B_SPLINE_CURVE((2.25967331459555,2.25967331459555,2.09743606996414))
REPRESENTATION_ITEM('')
) ;
#775=(
BOUNDED_CURVE()
B_SPLINE_CURVE(2,(#48561,#48562,#48563),.UNSPECIFIED.,.F.,.F.)
B_SPLINE_CURVE_WITH_KNOTS((3,3),(0.647835475111388,1.01047077031707),
 .UNSPECIFIED.)
CURVE()
GEOMETRIC_REPRESENTATION_ITEM()
RATIONAL_B_SPLINE_CURVE((2.09743606997569,2.25967331459555,2.25967331459555))
REPRESENTATION_ITEM('')
) ;
#776=(
BOUNDED_CURVE()
B_SPLINE_CURVE(2,(#48565,#48566,#48567),.UNSPECIFIED.,.F.,.F.)
B_SPLINE_CURVE_WITH_KNOTS((3,3),(-1.37310606553565,-1.01047077031707),
 .UNSPECIFIED.)
CURVE()
GEOMETRIC_REPRESENTATION_ITEM()
RATIONAL_B_SPLINE_CURVE((2.09743606996414,2.25967331459555,2.25967331459555))
REPRESENTATION_ITEM('')
) ;
#777=(
BOUNDED_CURVE()
B_SPLINE_CURVE(2,(#48569,#48570,#48571),.UNSPECIFIED.,.F.,.F.)
B_SPLINE_CURVE_WITH_KNOTS((3,3),(0.647835475111436,1.01047077031707),
 .UNSPECIFIED.)
CURVE()
GEOMETRIC_REPRESENTATION_ITEM()
RATIONAL_B_SPLINE_CURVE((2.09743606997573,2.25967331459556,2.25967331459556))
REPRESENTATION_ITEM('')
) ;
#778=(
BOUNDED_CURVE()
B_SPLINE_CURVE(2,(#48574,#48575,#48576),.UNSPECIFIED.,.F.,.F.)
B_SPLINE_CURVE_WITH_KNOTS((3,3),(-1.01047077031707,-0.647835475111437),
 .UNSPECIFIED.)
CURVE()
GEOMETRIC_REPRESENTATION_ITEM()
RATIONAL_B_SPLINE_CURVE((2.25967331459556,2.25967331459556,2.09743606997574))
REPRESENTATION_ITEM('')
) ;
#779=(
BOUNDED_CURVE()
B_SPLINE_CURVE(2,(#48579,#48580,#48581),.UNSPECIFIED.,.F.,.F.)
B_SPLINE_CURVE_WITH_KNOTS((3,3),(1.01047077031707,1.37310606553565),
 .UNSPECIFIED.)
CURVE()
GEOMETRIC_REPRESENTATION_ITEM()
RATIONAL_B_SPLINE_CURVE((2.25967331459556,2.25967331459556,2.09743606996414))
REPRESENTATION_ITEM('')
) ;
#780=(
BOUNDED_CURVE()
B_SPLINE_CURVE(2,(#48584,#48585,#48586),.UNSPECIFIED.,.F.,.F.)
B_SPLINE_CURVE_WITH_KNOTS((3,3),(-1.37310606553565,-1.01047077031707),
 .UNSPECIFIED.)
CURVE()
GEOMETRIC_REPRESENTATION_ITEM()
RATIONAL_B_SPLINE_CURVE((2.09743606996414,2.25967331459555,2.25967331459555))
REPRESENTATION_ITEM('')
) ;
#781=(
BOUNDED_CURVE()
B_SPLINE_CURVE(2,(#48588,#48589,#48590),.UNSPECIFIED.,.F.,.F.)
B_SPLINE_CURVE_WITH_KNOTS((3,3),(-1.01047077031707,-0.647835475111435),
 .UNSPECIFIED.)
CURVE()
GEOMETRIC_REPRESENTATION_ITEM()
RATIONAL_B_SPLINE_CURVE((2.25967331459555,2.25967331459555,2.09743606997573))
REPRESENTATION_ITEM('')
) ;
#782=(
BOUNDED_CURVE()
B_SPLINE_CURVE(2,(#48593,#48594,#48595),.UNSPECIFIED.,.F.,.F.)
B_SPLINE_CURVE_WITH_KNOTS((3,3),(1.01047077031706,1.37310606553565),
 .UNSPECIFIED.)
CURVE()
GEOMETRIC_REPRESENTATION_ITEM()
RATIONAL_B_SPLINE_CURVE((2.25967331459556,2.25967331459556,2.09743606996414))
REPRESENTATION_ITEM('')
) ;
#783=(
BOUNDED_CURVE()
B_SPLINE_CURVE(2,(#48596,#48597,#48598),.UNSPECIFIED.,.F.,.F.)
B_SPLINE_CURVE_WITH_KNOTS((3,3),(0.647835475111437,1.01047077031706),
 .UNSPECIFIED.)
CURVE()
GEOMETRIC_REPRESENTATION_ITEM()
RATIONAL_B_SPLINE_CURVE((2.09743606997574,2.25967331459556,2.25967331459556))
REPRESENTATION_ITEM('')
) ;
#784=(
BOUNDED_CURVE()
B_SPLINE_CURVE(2,(#48601,#48602,#48603),.UNSPECIFIED.,.F.,.F.)
B_SPLINE_CURVE_WITH_KNOTS((3,3),(-1.37310606553565,-1.01047077031706),
 .UNSPECIFIED.)
CURVE()
GEOMETRIC_REPRESENTATION_ITEM()
RATIONAL_B_SPLINE_CURVE((2.09743606996413,2.25967331459555,2.25967331459555))
REPRESENTATION_ITEM('')
) ;
#785=(
BOUNDED_CURVE()
B_SPLINE_CURVE(2,(#48604,#48605,#48606),.UNSPECIFIED.,.F.,.F.)
B_SPLINE_CURVE_WITH_KNOTS((3,3),(-1.01047077031706,-0.647835475111436),
 .UNSPECIFIED.)
CURVE()
GEOMETRIC_REPRESENTATION_ITEM()
RATIONAL_B_SPLINE_CURVE((2.25967331459555,2.25967331459555,2.09743606997573))
REPRESENTATION_ITEM('')
) ;
#786=(
BOUNDED_CURVE()
B_SPLINE_CURVE(2,(#48607,#48608,#48609),.UNSPECIFIED.,.F.,.F.)
B_SPLINE_CURVE_WITH_KNOTS((3,3),(1.01047077031706,1.37310606553565),
 .UNSPECIFIED.)
CURVE()
GEOMETRIC_REPRESENTATION_ITEM()
RATIONAL_B_SPLINE_CURVE((2.25967331459555,2.25967331459555,2.09743606996413))
REPRESENTATION_ITEM('')
) ;
#787=(
BOUNDED_CURVE()
B_SPLINE_CURVE(2,(#48610,#48611,#48612),.UNSPECIFIED.,.F.,.F.)
B_SPLINE_CURVE_WITH_KNOTS((3,3),(0.647835475111436,1.01047077031706),
 .UNSPECIFIED.)
CURVE()
GEOMETRIC_REPRESENTATION_ITEM()
RATIONAL_B_SPLINE_CURVE((2.09743606997573,2.25967331459555,2.25967331459555))
REPRESENTATION_ITEM('')
) ;
#815=SHAPE_REPRESENTATION_RELATIONSHIP('SRR','None',#86456,#827) ;
#827=ADVANCED_BREP_SHAPE_REPRESENTATION('',(#851),#86310) ;
#839=STYLED_ITEM('',(#86582),#851) ;
#851=MANIFOLD_SOLID_BREP('Body1',#32638) ;
#864=CONICAL_SURFACE('',#33078,1.5,0.78539816339745) ;
#865=CONICAL_SURFACE('',#33079,1.5,0.78539816339745) ;
#866=CONICAL_SURFACE('',#33080,1.5,0.78539816339745) ;
#867=CONICAL_SURFACE('',#33082,1.5,0.78539816339745) ;
#868=CONICAL_SURFACE('',#33086,2.75,1.0471975511966) ;
#869=CONICAL_SURFACE('',#33088,2.75,1.0471975511966) ;
#870=CONICAL_SURFACE('',#33108,2.75,1.0471975511966) ;
#871=CONICAL_SURFACE('',#33109,2.75,1.0471975511966) ;
#872=CONICAL_SURFACE('',#33110,2.75,1.0471975511966) ;
#873=CONICAL_SURFACE('',#33111,2.75,1.0471975511966) ;
#874=CONICAL_SURFACE('',#33112,2.75,1.0471975511966) ;
#875=CONICAL_SURFACE('',#33113,2.75,1.0471975511966) ;
#876=CONICAL_SURFACE('',#33114,2.75,1.0471975511966) ;
#877=CONICAL_SURFACE('',#33115,2.75,1.0471975511966) ;
#878=CONICAL_SURFACE('',#33116,2.75,1.0471975511966) ;
#879=CONICAL_SURFACE('',#33117,2.75,1.0471975511966) ;
#1048=FACE_BOUND('',#4356,.T.) ;
#1049=FACE_BOUND('',#4364,.T.) ;
#1193=B_SPLINE_CURVE_WITH_KNOTS('',3,(#47181,#47182,#47183,#47184,#47185,
#47186,#47187,#47188,#47189,#47190),.UNSPECIFIED.,.F.,.F.,(4,2,2,2,4),(3.31842937808031,
3.35016755864468,3.396837923606,3.44175906248201,3.48648133511502),
 .UNSPECIFIED.) ;
#1194=B_SPLINE_CURVE_WITH_KNOTS('',3,(#47193,#47194,#47195,#47196,#47197,
#47198,#47199,#47200,#47201,#47202,#47203,#47204,#47205,#47206),
 .UNSPECIFIED.,.F.,.F.,(4,2,2,2,2,2,4),(0.,0.0410648441701088,0.087038006677358,
0.133890124936013,0.178670683243025,0.225128281986789,0.260876372449635),
 .UNSPECIFIED.) ;
#1195=B_SPLINE_CURVE_WITH_KNOTS('',3,(#47211,#47212,#47213,#47214,#47215,
#47216,#47217,#47218,#47219,#47220,#47221,#47222,#47223,#47224,#47225,#47226,
#47227,#47228,#47229,#47230,#47231,#47232,#47233,#47234,#47235,#47236,#47237,
#47238,#47239,#47240,#47241,#47242,#47243,#47244,#47245,#47246),
 .UNSPECIFIED.,.F.,.F.,(4,2,2,2,2,2,2,2,2,2,2,2,2,2,2,2,2,4),(2.57674153154878,
2.61510934153612,2.66143878579143,2.70614655228561,2.75296429564827,2.79880209242763,
2.84382702777492,2.8909179029586,2.93622526800305,2.98243368493191,3.02891741450234,
3.07371420452932,3.12056663647033,3.1665682661734,3.211499121418,3.25876850942625,
3.30424075672643,3.31842937808031),.UNSPECIFIED.) ;
#1196=B_SPLINE_CURVE_WITH_KNOTS('',3,(#47247,#47248,#47249,#47250,#47251,
#47252,#47253,#47254,#47255,#47256,#47257,#47258,#47259,#47260,#47261,#47262,
#47263,#47264,#47265,#47266,#47267,#47268,#47269,#47270,#47271,#47272,#47273,
#47274,#47275,#47276,#47277,#47278,#47279,#47280,#47281,#47282),
 .UNSPECIFIED.,.F.,.F.,(4,2,2,2,2,2,2,2,2,2,2,2,2,2,2,2,2,4),(0.260876372449635,
0.271419194700287,0.316705310163363,0.363772652894618,0.408838431413797,
0.454655510522189,0.50148068321131,0.546189410353657,0.59250008742341,0.639168445054,
0.684332831326177,0.731267564232706,0.776520489163937,0.822218852479091,
0.869051231455086,0.913765477568226,0.959965017786808,1.00233576817236),
 .UNSPECIFIED.) ;
#1197=B_SPLINE_CURVE_WITH_KNOTS('',3,(#47287,#47288,#47289,#47290,#47291,
#47292,#47293,#47294,#47295,#47296,#47297,#47298,#47299,#47300,#47301,#47302,
#47303,#47304,#47305,#47306,#47307,#47308,#47309,#47310,#47311,#47312,#47313,
#47314,#47315,#47316,#47317,#47318,#47319,#47320,#47321,#47322),
 .UNSPECIFIED.,.F.,.F.,(4,2,2,2,2,2,2,2,2,2,2,2,2,2,2,2,2,4),(1.83527394228767,
1.88005636343276,1.92618554035068,1.97094346323703,2.01779361772358,2.06341660574272,
2.1088504927414,2.15569904695649,2.20078442257148,2.2477789890551,2.29398931205669,
2.33868626489989,2.38550400171857,2.43121478880165,2.47641117263732,2.52336103019069,
2.56853877611464,2.57674153154878),.UNSPECIFIED.) ;
#1198=B_SPLINE_CURVE_WITH_KNOTS('',3,(#47323,#47324,#47325,#47326,#47327,
#47328,#47329,#47330,#47331,#47332,#47333,#47334,#47335,#47336,#47337,#47338,
#47339,#47340,#47341,#47342,#47343,#47344,#47345,#47346,#47347,#47348,#47349,
#47350,#47351,#47352,#47353,#47354,#47355,#47356,#47357,#47358,#47359,#47360),
 .UNSPECIFIED.,.F.,.F.,(4,2,2,2,2,2,2,2,2,2,2,2,2,2,2,2,2,2,4),(1.00233576817236,
1.00706798297321,1.05214831718699,1.09899061505082,1.14449303921197,1.19011236551882,
1.23698396348855,1.28177341314926,1.32790037311896,1.37475812257317,1.4197708130612,
1.46653772846629,1.51240885912924,1.55796961908873,1.60533369336509,1.65027263764824,
1.69636292389366,1.7432590420322,1.74485974249583),.UNSPECIFIED.) ;
#1199=B_SPLINE_CURVE_WITH_KNOTS('',3,(#47365,#47366,#47367,#47368,#47369,
#47370,#47371,#47372,#47373,#47374,#47375,#47376,#47377,#47378,#47379,#47380,
#47381,#47382,#47383,#47384,#47385,#47386,#47387,#47388,#47389,#47390,#47391,
#47392,#47393,#47394,#47395,#47396,#47397,#47398,#47399,#47400,#47401,#47402),
 .UNSPECIFIED.,.F.,.F.,(4,2,2,2,2,2,2,2,2,2,2,2,2,2,2,2,2,2,4),(1.09311325644766,
1.09847320345976,1.14356176541002,1.1904136830288,1.23584708927346,1.28147323113724,
1.32832534251677,1.37308461796146,1.41921690762957,1.46605634177153,1.51107118762394,
1.55784129736534,1.60362255713177,1.64918322667193,1.69654896763227,1.74143993730663,
1.78820699300995,1.83321894472862,1.83527394228767),.UNSPECIFIED.) ;
#1200=B_SPLINE_CURVE_WITH_KNOTS('',3,(#47403,#47404,#47405,#47406,#47407,
#47408,#47409,#47410,#47411,#47412,#47413,#47414,#47415,#47416,#47417,#47418,
#47419,#47420,#47421,#47422,#47423,#47424,#47425,#47426,#47427,#47428,#47429,
#47430,#47431,#47432,#47433,#47434,#47435,#47436,#47437,#47438),
 .UNSPECIFIED.,.F.,.F.,(4,2,2,2,2,2,2,2,2,2,2,2,2,2,2,2,2,4),(1.74485974249583,
1.79012023382528,1.83625688485754,1.881046044964,1.92792078440463,1.97355010886049,
2.01904189360249,2.06589517212617,2.11098579935953,2.15806712470955,2.20427882402216,
2.24899676761857,2.29583421166923,2.34154509588437,2.38679067187208,2.43373894168524,
2.47891601834838,2.4866650924994),.UNSPECIFIED.) ;
#1201=B_SPLINE_CURVE_WITH_KNOTS('',3,(#47444,#47445,#47446,#47447,#47448,
#47449,#47450,#47451,#47452,#47453,#47454,#47455,#47456,#47457),
 .UNSPECIFIED.,.F.,.F.,(4,2,2,2,2,2,4),(3.22852173666992,3.26076961433847,
3.30742587418507,3.3523750214278,3.39930257668415,3.44548606230632,3.48984669211956),
 .UNSPECIFIED.) ;
#1202=B_SPLINE_CURVE_WITH_KNOTS('',3,(#47460,#47461,#47462,#47463,#47464,
#47465,#47466,#47467,#47468,#47469,#47470,#47471,#47472,#47473,#47474,#47475,
#47476,#47477),.UNSPECIFIED.,.F.,.F.,(4,2,2,2,2,2,2,2,4),(9.99999983706711E-7,
0.0438977278136496,0.0877054255663695,0.132637957456045,0.178643873404191,
0.225499231392538,0.270299674020503,0.316787599511936,0.351767081365554),
 .UNSPECIFIED.) ;
#1203=B_SPLINE_CURVE_WITH_KNOTS('',3,(#47483,#47484,#47485,#47486,#47487,
#47488,#47489,#47490,#47491,#47492,#47493,#47494,#47495,#47496,#47497,#47498),
 .UNSPECIFIED.,.F.,.F.,(4,2,2,2,2,2,2,4),(-0.356839236286574,-0.318839138763554,
-0.259130427174361,-0.201661085069514,-0.141844076929324,-0.0829140522622169,
-0.0414114555033024,-9.99999994644174E-7),.UNSPECIFIED.) ;
#1204=B_SPLINE_CURVE_WITH_KNOTS('',3,(#47501,#47502,#47503,#47504,#47505,
#47506,#47507,#47508,#47509,#47510,#47511,#47512,#47513,#47514,#47515,#47516,
#47517,#47518,#47519,#47520),.UNSPECIFIED.,.F.,.F.,(4,2,2,2,2,2,2,2,2,4),
(-5.6777690195579,-5.63616767911395,-5.59310905687254,-5.53347115580099,
-5.47651899265005,-5.41771065230489,-5.35758701805482,-5.30022347326295,
-5.24061901702306,-5.20527205396992),.UNSPECIFIED.) ;
#1205=B_SPLINE_CURVE_WITH_KNOTS('',3,(#47525,#47526,#47527,#47528,#47529,
#47530,#47531,#47532,#47533,#47534,#47535,#47536,#47537,#47538,#47539,#47540,
#47541,#47542,#47543,#47544,#47545,#47546,#47547,#47548,#47549,#47550,#47551,
#47552,#47553,#47554,#47555,#47556,#47557,#47558,#47559,#47560),
 .UNSPECIFIED.,.F.,.F.,(4,2,2,2,2,2,2,2,2,2,2,2,2,2,2,2,2,4),(-1.30494350966952,
-1.25776789010065,-1.1985119263168,-1.14137951639351,-1.08158575215186,
-1.0229769527965,-0.965565001793067,-0.905333721448379,-0.847397764355833,
-0.788595538964929,-0.729125616520127,-0.671843999206589,-0.612011464665177,
-0.553186058070021,-0.495885382179051,-0.435418594272755,-0.377269758491555,
-0.356839236286574),.UNSPECIFIED.) ;
#1206=B_SPLINE_CURVE_WITH_KNOTS('',3,(#47561,#47562,#47563,#47564,#47565,
#47566,#47567,#47568,#47569,#47570,#47571,#47572,#47573,#47574,#47575,#47576,
#47577,#47578,#47579,#47580,#47581,#47582,#47583,#47584,#47585,#47586,#47587,
#47588,#47589,#47590,#47591,#47592,#47593,#47594,#47595,#47596),
 .UNSPECIFIED.,.F.,.F.,(4,2,2,2,2,2,2,2,2,2,2,2,2,2,2,2,2,4),(-5.20527205396992,
-5.18260211509116,-5.1245647406915,-5.06488837094347,-5.00783480509734,
-4.94914569176594,-4.88949082733128,-4.8322501268223,-4.77278429618413,
-4.71425928615259,-4.65633638196459,-4.59611265214601,-4.53886176529339,
-4.48026581636814,-4.4205639465445,-4.36347931260193,-4.30423839363068,
-4.25917338249842),.UNSPECIFIED.) ;
#1207=B_SPLINE_CURVE_WITH_KNOTS('',3,(#47601,#47602,#47603,#47604,#47605,
#47606,#47607,#47608,#47609,#47610,#47611,#47612,#47613,#47614,#47615,#47616,
#47617,#47618,#47619,#47620,#47621,#47622,#47623,#47624,#47625,#47626,#47627,
#47628,#47629,#47630,#47631,#47632,#47633,#47634,#47635,#47636),
 .UNSPECIFIED.,.F.,.F.,(4,2,2,2,2,2,2,2,2,2,2,2,2,2,2,2,2,4),(-2.25248934816888,
-2.19617623781344,-2.13725183863766,-2.08012580789218,-2.02032048864309,
-1.96204771939477,-1.904125144753,-1.84426787577856,-1.78666784944015,-1.72681573103074,
-1.66774351387222,-1.61066141331469,-1.55087592498769,-1.49245308352448,
-1.43482961561388,-1.37480327574036,-1.31705178913088,-1.30494350966952),
 .UNSPECIFIED.) ;
#1208=B_SPLINE_CURVE_WITH_KNOTS('',3,(#47637,#47638,#47639,#47640,#47641,
#47642,#47643,#47644,#47645,#47646,#47647,#47648,#47649,#47650,#47651,#47652,
#47653,#47654,#47655,#47656,#47657,#47658,#47659,#47660,#47661,#47662,#47663,
#47664,#47665,#47666,#47667,#47668,#47669,#47670,#47671,#47672),
 .UNSPECIFIED.,.F.,.F.,(4,2,2,2,2,2,2,2,2,2,2,2,2,2,2,2,2,4),(-4.25917338249842,
-4.24527779180941,-4.18755180165972,-4.12754644710674,-4.070126508801,-4.01173002419351,
-3.95204920618323,-3.89505746671119,-3.83601367393912,-3.77651947097669,
-3.71895945267056,-3.6591389505398,-3.60145584791493,-3.54322523402684,
-3.48353646776607,-3.42654013249902,-3.36766003550048,-3.31332463994661),
 .UNSPECIFIED.) ;
#1209=B_SPLINE_CURVE_WITH_KNOTS('',3,(#47677,#47678,#47679,#47680,#47681,
#47682,#47683,#47684,#47685,#47686,#47687,#47688,#47689,#47690,#47691,#47692,
#47693,#47694,#47695,#47696,#47697,#47698,#47699,#47700,#47701,#47702,#47703,
#47704,#47705,#47706,#47707,#47708,#47709,#47710,#47711,#47712,#47713,#47714),
 .UNSPECIFIED.,.F.,.F.,(4,2,2,2,2,2,2,2,2,2,2,2,2,2,2,2,2,2,4),(-3.20029950146654,
-3.19315660740551,-3.13560653382823,-3.07580344967673,-3.01782963552705,
-2.95960638292588,-2.89981630259394,-2.84269176491814,-2.78323065019205,
-2.72595980442964,-2.66615935009437,-2.60734191496364,-2.55008635989913,
-2.4896261022618,-2.43148541093545,-2.3731342360459,-2.31343130070289,-2.25596874753601,
-2.25248934816888),.UNSPECIFIED.) ;
#1210=B_SPLINE_CURVE_WITH_KNOTS('',3,(#47715,#47716,#47717,#47718,#47719,
#47720,#47721,#47722,#47723,#47724,#47725,#47726,#47727,#47728,#47729,#47730,
#47731,#47732,#47733,#47734,#47735,#47736,#47737,#47738,#47739,#47740,#47741,
#47742,#47743,#47744,#47745,#47746,#47747,#47748,#47749,#47750,#47751,#47752),
 .UNSPECIFIED.,.F.,.F.,(4,2,2,2,2,2,2,2,2,2,2,2,2,2,2,2,2,2,4),(-3.31332463994661,
-3.30756374577828,-3.25013416214204,-3.19045983715782,-3.1324387157978,
-3.0743354352636,-3.01461170216103,-2.95752404946368,-2.89876880763459,
-2.83906516495525,-2.77933159023642,-2.72059832312161,-2.6633956702534,
-2.60302322859973,-2.5449655288037,-2.48664210359268,-2.42702627164252,
-2.36964659357858,-2.36659114930348),.UNSPECIFIED.) ;
#1211=B_SPLINE_CURVE_WITH_KNOTS('',3,(#47757,#47758,#47759,#47760,#47761,
#47762,#47763,#47764,#47765,#47766,#47767,#47768,#47769,#47770,#47771,#47772,
#47773,#47774,#47775,#47776,#47777,#47778,#47779,#47780,#47781,#47782,#47783,
#47784,#47785,#47786,#47787,#47788,#47789,#47790,#47791,#47792),
 .UNSPECIFIED.,.F.,.F.,(4,2,2,2,2,2,2,2,2,2,2,2,2,2,2,2,2,4),(-4.14747208700764,
-4.13206742370891,-4.07419594267165,-4.01403463010671,-3.95660744642544,
-3.8980639186862,-3.83829740608844,-3.78120614155281,-3.72201520284988,
-3.66263824916934,-3.6049444685612,-3.54498075518231,-3.48732198039695,
-3.42895705995953,-3.36919260172769,-3.31213058552288,-3.25311607462449,
-3.20029950146654),.UNSPECIFIED.) ;
#1212=B_SPLINE_CURVE_WITH_KNOTS('',3,(#47793,#47794,#47795,#47796,#47797,
#47798,#47799,#47800,#47801,#47802,#47803,#47804,#47805,#47806,#47807,#47808,
#47809,#47810,#47811,#47812,#47813,#47814,#47815,#47816,#47817,#47818,#47819,
#47820,#47821,#47822,#47823,#47824,#47825,#47826,#47827,#47828),
 .UNSPECIFIED.,.F.,.F.,(4,2,2,2,2,2,2,2,2,2,2,2,2,2,2,2,2,4),(-2.36659114930348,
-2.3099267325564,-2.2510883534928,-2.19402473111864,-2.1342907007857,-2.07610338007785,
-2.0182197874013,-1.95845180936089,-1.90093669275898,-1.84109983357991,
-1.78211765323279,-1.72510653073043,-1.66539497500452,-1.60706157178376,
-1.54948423504781,-1.48955121115931,-1.43188832707264,-1.42020742457329),
 .UNSPECIFIED.) ;
#1213=B_SPLINE_CURVE_WITH_KNOTS('',3,(#47834,#47835,#47836,#47837,#47838,
#47839,#47840,#47841,#47842,#47843,#47844,#47845,#47846,#47847,#47848,#47849,
#47850,#47851,#47852,#47853),.UNSPECIFIED.,.F.,.F.,(4,2,2,2,2,2,2,2,2,4),
(-0.473361116390324,-0.434980285469829,-0.375370649937796,-0.317995768158978,
-0.258264150217988,-0.199432012735734,-0.142347766489119,-0.0826003210214793,
-0.0405758598073532,-9.99999995310308E-7),.UNSPECIFIED.) ;
#1214=B_SPLINE_CURVE_WITH_KNOTS('',3,(#47856,#47857,#47858,#47859,#47860,
#47861,#47862,#47863,#47864,#47865,#47866,#47867,#47868,#47869,#47870,#47871,
#47872,#47873,#47874,#47875,#47876,#47877,#47878,#47879),.UNSPECIFIED.,
 .F.,.F.,(4,2,2,2,2,2,2,2,2,2,2,4),(-5.68568308835527,-5.64187567407348,
-5.59831170654822,-5.54062509920359,-5.48228578877153,-5.422526237897,-5.36546755897281,
-5.3064784656501,-5.2464513100281,-5.18892242603572,-5.12914260288557,-5.09523963172672),
 .UNSPECIFIED.) ;
#1215=B_SPLINE_CURVE_WITH_KNOTS('',3,(#47884,#47885,#47886,#47887),
 .UNSPECIFIED.,.F.,.F.,(4,4),(-1.00218290968104,-0.991970784037339),
 .UNSPECIFIED.) ;
#1216=B_SPLINE_CURVE_WITH_KNOTS('',3,(#47888,#47889,#47890,#47891,#47892,
#47893,#47894,#47895),.UNSPECIFIED.,.F.,.F.,(4,2,2,4),(0.,0.0435785122875659,
0.0903817076613929,0.124172560080924),.UNSPECIFIED.) ;
#1217=B_SPLINE_CURVE_WITH_KNOTS('',3,(#47899,#47900,#47901,#47902,#47903,
#47904,#47905,#47906),.UNSPECIFIED.,.F.,.F.,(4,2,2,4),(-0.575278937572396,
-0.559414249044956,-0.544216358804097,-0.536951818658365),.UNSPECIFIED.) ;
#1218=B_SPLINE_CURVE_WITH_KNOTS('',3,(#47907,#47908,#47909,#47910,#47911,
#47912,#47913,#47914,#47915,#47916,#47917,#47918,#47919,#47920),
 .UNSPECIFIED.,.F.,.F.,(4,2,2,2,2,2,4),(-0.166734145007444,-0.148557002683626,
-0.136251466347306,-0.113028859542707,-0.0847672793749983,-0.0413426304955296,
-1.00000017441704E-6),.UNSPECIFIED.) ;
#1219=B_SPLINE_CURVE_WITH_KNOTS('',3,(#47923,#47924,#47925,#47926,#47927,
#47928,#47929,#47930,#47931,#47932,#47933,#47934,#47935,#47936,#47937,#47938,
#47939,#47940,#47941,#47942,#47943,#47944,#47945,#47946,#47947,#47948,#47949,
#47950,#47951,#47952,#47953,#47954,#47955,#47956,#47957,#47958),
 .UNSPECIFIED.,.F.,.F.,(4,2,2,2,2,2,2,2,2,2,2,2,2,2,2,2,2,4),(-0.536951818658365,
-0.536175700978615,-0.519496434514374,-0.503627636028881,-0.482751345818568,
-0.453972299702605,-0.427124357976038,-0.412423739643194,-0.382270815269358,
-0.353759615123692,-0.315266001158416,-0.260624023001414,-0.205656350189048,
-0.177984976990091,-0.12376571829927,-0.0654292820557721,-0.0322025263864932,
-1.00000009040091E-6),.UNSPECIFIED.) ;
#1220=B_SPLINE_CURVE_WITH_KNOTS('',3,(#47960,#47961,#47962,#47963,#47964,
#47965,#47966,#47967),.UNSPECIFIED.,.F.,.F.,(4,2,2,4),(0.124172560080924,
0.157998858836025,0.240075000933573,0.324188312978485),.UNSPECIFIED.) ;
#1221=B_SPLINE_CURVE_WITH_KNOTS('',3,(#47969,#47970,#47971,#47972,#47973,
#47974,#47975,#47976,#47977,#47978,#47979,#47980,#47981,#47982,#47983,#47984,
#47985,#47986,#47987,#47988,#47989,#47990,#47991,#47992,#47993,#47994,#47995,
#47996,#47997,#47998,#47999,#48000,#48001,#48002,#48003,#48004,#48005,#48006,
#48007,#48008),.UNSPECIFIED.,.F.,.F.,(4,2,2,2,2,2,2,2,2,2,2,2,2,2,2,2,2,
2,2,4),(-0.991970784037339,-0.976482169541418,-0.940511015363057,-0.898601131647801,
-0.876476528706804,-0.830559860454117,-0.786858882019556,-0.729757356509824,
-0.65196076520893,-0.579389748760059,-0.491285302902488,-0.394350008062906,
-0.294163274796139,-0.237450467655031,-0.191239556405745,-0.16841211518385,
-0.117188759032826,-0.0606892948336317,-0.0314347233699885,-1.00000009273238E-6),
 .UNSPECIFIED.) ;
#1222=B_SPLINE_CURVE_WITH_KNOTS('',3,(#48010,#48011,#48012,#48013,#48014,
#48015,#48016,#48017,#48018,#48019,#48020,#48021,#48022,#48023,#48024,#48025,
#48026,#48027,#48028,#48029,#48030,#48031,#48032,#48033,#48034,#48035,#48036,
#48037,#48038,#48039,#48040,#48041,#48042,#48043,#48044,#48045),
 .UNSPECIFIED.,.F.,.F.,(4,2,2,2,2,2,2,2,2,2,2,2,2,2,2,2,2,4),(-5.09523963172672,
-5.07113258312941,-5.01293004439165,-4.95314154316727,-4.89601012144808,
-4.83715542661164,-4.77738423908235,-4.71998612925933,-4.6603534598268,
-4.60187538467476,-4.54379684525718,-4.48340624898908,-4.42611243528161,
-4.36735853154431,-4.30756005089831,-4.2503406903036,-4.19094189274728,
-4.14747208700764),.UNSPECIFIED.) ;
#1223=B_SPLINE_CURVE_WITH_KNOTS('',3,(#48046,#48047,#48048,#48049,#48050,
#48051,#48052,#48053,#48054,#48055,#48056,#48057,#48058,#48059,#48060,#48061,
#48062,#48063,#48064,#48065,#48066,#48067,#48068,#48069,#48070,#48071,#48072,
#48073,#48074,#48075,#48076,#48077,#48078,#48079,#48080,#48081),
 .UNSPECIFIED.,.F.,.F.,(4,2,2,2,2,2,2,2,2,2,2,2,2,2,2,2,2,4),(-1.42020742457329,
-1.37262582777851,-1.31346342085115,-1.25641173589597,-1.19669477961086,
-1.13817895843239,-1.08082218003548,-1.02068777127858,-0.962843692323244,
-0.904072038294528,-0.844698668720221,-0.787507583204744,-0.727755034178589,
-0.669025666660467,-0.611790195274486,-0.551423357069376,-0.493369273141207,
-0.473361116390324),.UNSPECIFIED.) ;
#1224=B_SPLINE_CURVE_WITH_KNOTS('',3,(#48083,#48084,#48085,#48086,#48087,
#48088,#48089,#48090,#48091,#48092,#48093,#48094,#48095,#48096,#48097,#48098,
#48099,#48100,#48101,#48102,#48103,#48104,#48105,#48106,#48107,#48108,#48109,
#48110,#48111,#48112,#48113,#48114,#48115,#48116,#48117,#48118),
 .UNSPECIFIED.,.F.,.F.,(4,2,2,2,2,2,2,2,2,2,2,2,2,2,2,2,2,4),(0.351767081365554,
0.362994825087978,0.408306200866931,0.45540131847049,0.500427176257259,
0.546268992971341,0.593089400650884,0.63780007653961,0.684133472260792,
0.730702175568153,0.775883529775975,0.822837200812743,0.868033712567382,
0.913748097481785,0.960568133215132,1.00526716490256,1.05148103368736,1.09311325644766),
 .UNSPECIFIED.) ;
#1225=B_SPLINE_CURVE_WITH_KNOTS('',3,(#48119,#48120,#48121,#48122,#48123,
#48124,#48125,#48126,#48127,#48128,#48129,#48130,#48131,#48132,#48133,#48134,
#48135,#48136,#48137,#48138,#48139,#48140,#48141,#48142,#48143,#48144,#48145,
#48146,#48147,#48148,#48149,#48150,#48151,#48152,#48153,#48154),
 .UNSPECIFIED.,.F.,.F.,(4,2,2,2,2,2,2,2,2,2,2,2,2,2,2,2,2,4),(2.4866650924994,
2.52556556364955,2.57189071243123,2.61660775868172,2.66344004151552,2.7092720422196,
2.75433484706525,2.80141816191296,2.84671925205663,2.89299554386376,2.93946975715054,
2.98426354830769,3.03112497725156,3.07711531442473,3.12207147536806,3.16932769067158,
3.21478837165691,3.22852173666992),.UNSPECIFIED.) ;
#1752=PLANE('',#33090) ;
#1753=PLANE('',#33096) ;
#1754=PLANE('',#33097) ;
#1755=PLANE('',#33098) ;
#1756=PLANE('',#33099) ;
#1757=PLANE('',#33100) ;
#1758=PLANE('',#33101) ;
#1759=PLANE('',#33102) ;
#2398=FACE_OUTER_BOUND('',#4334,.T.) ;
#2399=FACE_OUTER_BOUND('',#4335,.T.) ;
#2400=FACE_OUTER_BOUND('',#4336,.T.) ;
#2401=FACE_OUTER_BOUND('',#4337,.T.) ;
#2402=FACE_OUTER_BOUND('',#4338,.T.) ;
#2403=FACE_OUTER_BOUND('',#4339,.T.) ;
#2404=FACE_OUTER_BOUND('',#4340,.T.) ;
#2405=FACE_OUTER_BOUND('',#4341,.T.) ;
#2406=FACE_OUTER_BOUND('',#4342,.T.) ;
#2407=FACE_OUTER_BOUND('',#4343,.T.) ;
#2408=FACE_OUTER_BOUND('',#4344,.T.) ;
#2409=FACE_OUTER_BOUND('',#4345,.T.) ;
#2410=FACE_OUTER_BOUND('',#4346,.T.) ;
#2411=FACE_OUTER_BOUND('',#4347,.T.) ;
#2412=FACE_OUTER_BOUND('',#4348,.T.) ;
#2413=FACE_OUTER_BOUND('',#4349,.T.) ;
#2414=FACE_OUTER_BOUND('',#4350,.T.) ;
#2415=FACE_OUTER_BOUND('',#4351,.T.) ;
#2416=FACE_OUTER_BOUND('',#4352,.T.) ;
#2417=FACE_OUTER_BOUND('',#4353,.T.) ;
#2418=FACE_OUTER_BOUND('',#4354,.T.) ;
#2419=FACE_OUTER_BOUND('',#4355,.T.) ;
#2420=FACE_OUTER_BOUND('',#4357,.T.) ;
#2421=FACE_OUTER_BOUND('',#4358,.T.) ;
#2422=FACE_OUTER_BOUND('',#4359,.T.) ;
#2423=FACE_OUTER_BOUND('',#4360,.T.) ;
#2424=FACE_OUTER_BOUND('',#4361,.T.) ;
#2425=FACE_OUTER_BOUND('',#4362,.T.) ;
#2426=FACE_OUTER_BOUND('',#4363,.T.) ;
#2427=FACE_OUTER_BOUND('',#4365,.T.) ;
#2428=FACE_OUTER_BOUND('',#4366,.T.) ;
#2429=FACE_OUTER_BOUND('',#4367,.T.) ;
#2430=FACE_OUTER_BOUND('',#4368,.T.) ;
#2431=FACE_OUTER_BOUND('',#4369,.T.) ;
#2432=FACE_OUTER_BOUND('',#4370,.T.) ;
#2433=FACE_OUTER_BOUND('',#4371,.T.) ;
#2434=FACE_OUTER_BOUND('',#4372,.T.) ;
#2435=FACE_OUTER_BOUND('',#4373,.T.) ;
#2436=FACE_OUTER_BOUND('',#4374,.T.) ;
#4334=EDGE_LOOP('',(#21124,#21125,#21126,#21127)) ;
#4335=EDGE_LOOP('',(#21128,#21129,#21130,#21131)) ;
#4336=EDGE_LOOP('',(#21132,#21133,#21134,#21135)) ;
#4337=EDGE_LOOP('',(#21136,#21137,#21138,#21139)) ;
#4338=EDGE_LOOP('',(#21140,#21141,#21142,#21143)) ;
#4339=EDGE_LOOP('',(#21144,#21145,#21146,#21147)) ;
#4340=EDGE_LOOP('',(#21148,#21149,#21150,#21151)) ;
#4341=EDGE_LOOP('',(#21152,#21153,#21154,#21155)) ;
#4342=EDGE_LOOP('',(#21156,#21157,#21158,#21159)) ;
#4343=EDGE_LOOP('',(#21160,#21161,#21162,#21163)) ;
#4344=EDGE_LOOP('',(#21164,#21165,#21166,#21167)) ;
#4345=EDGE_LOOP('',(#21168,#21169,#21170,#21171)) ;
#4346=EDGE_LOOP('',(#21172,#21173,#21174,#21175)) ;
#4347=EDGE_LOOP('',(#21176,#21177,#21178)) ;
#4348=EDGE_LOOP('',(#21179,#21180,#21181,#21182)) ;
#4349=EDGE_LOOP('',(#21183,#21184,#21185,#21186)) ;
#4350=EDGE_LOOP('',(#21187,#21188,#21189,#21190)) ;
#4351=EDGE_LOOP('',(#21191,#21192,#21193)) ;
#4352=EDGE_LOOP('',(#21194,#21195,#21196)) ;
#4353=EDGE_LOOP('',(#21197,#21198,#21199,#21200,#21201,#21202,#21203,#21204,
#21205,#21206,#21207,#21208,#21209,#21210,#21211,#21212)) ;
#4354=EDGE_LOOP('',(#21213,#21214,#21215,#21216,#21217,#21218,#21219,#21220,
#21221,#21222,#21223,#21224,#21225,#21226,#21227,#21228,#21229)) ;
#4355=EDGE_LOOP('',(#21230,#21231,#21232,#21233,#21234,#21235)) ;
#4356=EDGE_LOOP('',(#21236,#21237)) ;
#4357=EDGE_LOOP('',(#21238,#21239,#21240,#21241,#21242,#21243)) ;
#4358=EDGE_LOOP('',(#21244,#21245,#21246,#21247,#21248,#21249)) ;
#4359=EDGE_LOOP('',(#21250,#21251,#21252,#21253,#21254,#21255)) ;
#4360=EDGE_LOOP('',(#21256,#21257,#21258,#21259,#21260,#21261)) ;
#4361=EDGE_LOOP('',(#21262,#21263,#21264,#21265,#21266,#21267)) ;
#4362=EDGE_LOOP('',(#21268,#21269,#21270,#21271,#21272,#21273)) ;
#4363=EDGE_LOOP('',(#21274,#21275,#21276,#21277,#21278,#21279)) ;
#4364=EDGE_LOOP('',(#21280,#21281)) ;
#4365=EDGE_LOOP('',(#21282,#21283,#21284)) ;
#4366=EDGE_LOOP('',(#21285,#21286,#21287)) ;
#4367=EDGE_LOOP('',(#21288,#21289,#21290)) ;
#4368=EDGE_LOOP('',(#21291,#21292,#21293)) ;
#4369=EDGE_LOOP('',(#21294,#21295,#21296)) ;
#4370=EDGE_LOOP('',(#21297,#21298,#21299)) ;
#4371=EDGE_LOOP('',(#21300,#21301,#21302)) ;
#4372=EDGE_LOOP('',(#21303,#21304,#21305)) ;
#4373=EDGE_LOOP('',(#21306,#21307,#21308)) ;
#4374=EDGE_LOOP('',(#21309,#21310,#21311)) ;
#6443=LINE('',#47179,#8762) ;
#6444=LINE('',#47210,#8763) ;
#6445=LINE('',#47286,#8764) ;
#6446=LINE('',#47364,#8765) ;
#6447=LINE('',#47442,#8766) ;
#6448=LINE('',#47481,#8767) ;
#6449=LINE('',#47524,#8768) ;
#6450=LINE('',#47600,#8769) ;
#6451=LINE('',#47676,#8770) ;
#6452=LINE('',#47756,#8771) ;
#6453=LINE('',#47832,#8772) ;
#6454=LINE('',#47883,#8773) ;
#6455=LINE('',#47898,#8774) ;
#6456=LINE('',#48530,#8775) ;
#6457=LINE('',#48540,#8776) ;
#6458=LINE('',#48557,#8777) ;
#6459=LINE('',#48568,#8778) ;
#6460=LINE('',#48578,#8779) ;
#6461=LINE('',#48592,#8780) ;
#8762=VECTOR('',#37317,1.17524047358083) ;
#8763=VECTOR('',#37322,1.17524047358083) ;
#8764=VECTOR('',#37325,1.17524047358083) ;
#8765=VECTOR('',#37328,1.17524047358083) ;
#8766=VECTOR('',#37331,1.17524047358083) ;
#8767=VECTOR('',#37336,1.5) ;
#8768=VECTOR('',#37341,1.5) ;
#8769=VECTOR('',#37344,1.5) ;
#8770=VECTOR('',#37347,1.5) ;
#8771=VECTOR('',#37350,1.5) ;
#8772=VECTOR('',#37353,1.5) ;
#8773=VECTOR('',#37358,1.5) ;
#8774=VECTOR('',#37361,1.5) ;
#8775=VECTOR('',#37396,1000.) ;
#8776=VECTOR('',#37397,1000.) ;
#8777=VECTOR('',#37400,1000.) ;
#8778=VECTOR('',#37403,1000.) ;
#8779=VECTOR('',#37406,1000.) ;
#8780=VECTOR('',#37409,1000.) ;
#11033=CIRCLE('',#33064,1.17524047358084) ;
#11034=CIRCLE('',#33069,1.17524047358083) ;
#11035=CIRCLE('',#33071,1.5) ;
#11036=CIRCLE('',#33077,1.5) ;
#11037=CIRCLE('',#33081,1.5) ;
#11038=CIRCLE('',#33083,1.5) ;
#11039=CIRCLE('',#33087,2.75) ;
#11040=CIRCLE('',#33089,2.75) ;
#11041=CIRCLE('',#33091,2.75) ;
#11042=CIRCLE('',#33092,2.75) ;
#11043=CIRCLE('',#33093,2.75) ;
#11044=CIRCLE('',#33094,2.75) ;
#11045=CIRCLE('',#33095,2.75) ;
#11046=CIRCLE('',#33103,2.75) ;
#11047=CIRCLE('',#33104,2.75) ;
#11048=CIRCLE('',#33105,2.75) ;
#11049=CIRCLE('',#33106,2.75) ;
#11050=CIRCLE('',#33107,2.75) ;
#12913=VERTEX_POINT('',#47177) ;
#12914=VERTEX_POINT('',#47178) ;
#12915=VERTEX_POINT('',#47180) ;
#12916=VERTEX_POINT('',#47191) ;
#12917=VERTEX_POINT('',#47208) ;
#12918=VERTEX_POINT('',#47209) ;
#12919=VERTEX_POINT('',#47284) ;
#12920=VERTEX_POINT('',#47285) ;
#12921=VERTEX_POINT('',#47362) ;
#12922=VERTEX_POINT('',#47363) ;
#12923=VERTEX_POINT('',#47440) ;
#12924=VERTEX_POINT('',#47441) ;
#12925=VERTEX_POINT('',#47443) ;
#12926=VERTEX_POINT('',#47458) ;
#12927=VERTEX_POINT('',#47479) ;
#12928=VERTEX_POINT('',#47480) ;
#12929=VERTEX_POINT('',#47482) ;
#12930=VERTEX_POINT('',#47499) ;
#12931=VERTEX_POINT('',#47522) ;
#12932=VERTEX_POINT('',#47523) ;
#12933=VERTEX_POINT('',#47598) ;
#12934=VERTEX_POINT('',#47599) ;
#12935=VERTEX_POINT('',#47674) ;
#12936=VERTEX_POINT('',#47675) ;
#12937=VERTEX_POINT('',#47754) ;
#12938=VERTEX_POINT('',#47755) ;
#12939=VERTEX_POINT('',#47830) ;
#12940=VERTEX_POINT('',#47831) ;
#12941=VERTEX_POINT('',#47833) ;
#12942=VERTEX_POINT('',#47854) ;
#12943=VERTEX_POINT('',#47881) ;
#12944=VERTEX_POINT('',#47882) ;
#12945=VERTEX_POINT('',#47897) ;
#12946=VERTEX_POINT('',#48156) ;
#12947=VERTEX_POINT('',#48157) ;
#12948=VERTEX_POINT('',#48159) ;
#12949=VERTEX_POINT('',#48167) ;
#12950=VERTEX_POINT('',#48168) ;
#12951=VERTEX_POINT('',#48170) ;
#12952=VERTEX_POINT('',#48518) ;
#12953=VERTEX_POINT('',#48520) ;
#12954=VERTEX_POINT('',#48522) ;
#12955=VERTEX_POINT('',#48524) ;
#12956=VERTEX_POINT('',#48528) ;
#12957=VERTEX_POINT('',#48529) ;
#12958=VERTEX_POINT('',#48531) ;
#12959=VERTEX_POINT('',#48535) ;
#12960=VERTEX_POINT('',#48539) ;
#12961=VERTEX_POINT('',#48548) ;
#12962=VERTEX_POINT('',#48552) ;
#12963=VERTEX_POINT('',#48556) ;
#12964=VERTEX_POINT('',#48573) ;
#12965=VERTEX_POINT('',#48577) ;
#12966=VERTEX_POINT('',#48583) ;
#12967=VERTEX_POINT('',#48587) ;
#12968=VERTEX_POINT('',#48591) ;
#12969=VERTEX_POINT('',#48600) ;
#15968=EDGE_CURVE('',#12913,#12914,#6443,.T.) ;
#15969=EDGE_CURVE('',#12914,#12915,#1193,.T.) ;
#15970=EDGE_CURVE('',#12915,#12916,#11033,.T.) ;
#15971=EDGE_CURVE('',#12913,#12916,#1194,.F.) ;
#15972=EDGE_CURVE('',#12917,#12918,#6444,.T.) ;
#15973=EDGE_CURVE('',#12918,#12914,#1195,.T.) ;
#15974=EDGE_CURVE('',#12917,#12913,#1196,.F.) ;
#15975=EDGE_CURVE('',#12919,#12920,#6445,.T.) ;
#15976=EDGE_CURVE('',#12920,#12918,#1197,.T.) ;
#15977=EDGE_CURVE('',#12919,#12917,#1198,.F.) ;
#15978=EDGE_CURVE('',#12921,#12922,#6446,.T.) ;
#15979=EDGE_CURVE('',#12922,#12920,#1199,.T.) ;
#15980=EDGE_CURVE('',#12921,#12919,#1200,.F.) ;
#15981=EDGE_CURVE('',#12923,#12924,#6447,.T.) ;
#15982=EDGE_CURVE('',#12925,#12923,#1201,.F.) ;
#15983=EDGE_CURVE('',#12926,#12925,#11034,.T.) ;
#15984=EDGE_CURVE('',#12926,#12924,#1202,.T.) ;
#15985=EDGE_CURVE('',#12927,#12928,#6448,.T.) ;
#15986=EDGE_CURVE('',#12929,#12928,#1203,.F.) ;
#15987=EDGE_CURVE('',#12930,#12929,#11035,.T.) ;
#15988=EDGE_CURVE('',#12927,#12930,#1204,.F.) ;
#15989=EDGE_CURVE('',#12931,#12932,#6449,.T.) ;
#15990=EDGE_CURVE('',#12928,#12932,#1205,.F.) ;
#15991=EDGE_CURVE('',#12931,#12927,#1206,.F.) ;
#15992=EDGE_CURVE('',#12933,#12934,#6450,.T.) ;
#15993=EDGE_CURVE('',#12932,#12934,#1207,.F.) ;
#15994=EDGE_CURVE('',#12933,#12931,#1208,.F.) ;
#15995=EDGE_CURVE('',#12935,#12936,#6451,.T.) ;
#15996=EDGE_CURVE('',#12934,#12936,#1209,.F.) ;
#15997=EDGE_CURVE('',#12935,#12933,#1210,.F.) ;
#15998=EDGE_CURVE('',#12937,#12938,#6452,.T.) ;
#15999=EDGE_CURVE('',#12936,#12938,#1211,.F.) ;
#16000=EDGE_CURVE('',#12937,#12935,#1212,.F.) ;
#16001=EDGE_CURVE('',#12939,#12940,#6453,.T.) ;
#16002=EDGE_CURVE('',#12941,#12939,#1213,.F.) ;
#16003=EDGE_CURVE('',#12941,#12942,#11036,.T.) ;
#16004=EDGE_CURVE('',#12940,#12942,#1214,.F.) ;
#16005=EDGE_CURVE('',#12943,#12944,#6454,.T.) ;
#16006=EDGE_CURVE('',#12943,#12926,#1215,.F.) ;
#16007=EDGE_CURVE('',#12925,#12944,#1216,.T.) ;
#16008=EDGE_CURVE('',#12945,#12930,#6455,.T.) ;
#16009=EDGE_CURVE('',#12916,#12945,#1217,.T.) ;
#16010=EDGE_CURVE('',#12930,#12915,#1218,.T.) ;
#16011=EDGE_CURVE('',#12929,#12930,#11037,.T.) ;
#16012=EDGE_CURVE('',#12945,#12929,#1219,.T.) ;
#16013=EDGE_CURVE('',#12944,#12942,#1220,.T.) ;
#16014=EDGE_CURVE('',#12942,#12941,#11038,.T.) ;
#16015=EDGE_CURVE('',#12941,#12943,#1221,.F.) ;
#16016=EDGE_CURVE('',#12938,#12940,#1222,.F.) ;
#16017=EDGE_CURVE('',#12939,#12937,#1223,.F.) ;
#16018=EDGE_CURVE('',#12924,#12922,#1224,.T.) ;
#16019=EDGE_CURVE('',#12923,#12921,#1225,.F.) ;
#16020=EDGE_CURVE('',#12946,#12947,#11039,.T.) ;
#16021=EDGE_CURVE('',#12948,#12946,#764,.T.) ;
#16022=EDGE_CURVE('',#12947,#12948,#765,.T.) ;
#16023=EDGE_CURVE('',#12949,#12950,#11040,.T.) ;
#16024=EDGE_CURVE('',#12949,#12951,#766,.T.) ;
#16025=EDGE_CURVE('',#12951,#12950,#767,.T.) ;
#16026=EDGE_CURVE('',#12950,#12952,#11041,.T.) ;
#16027=EDGE_CURVE('',#12952,#12953,#11042,.T.) ;
#16028=EDGE_CURVE('',#12953,#12954,#11043,.T.) ;
#16029=EDGE_CURVE('',#12954,#12955,#11044,.T.) ;
#16030=EDGE_CURVE('',#12955,#12949,#11045,.T.) ;
#16031=EDGE_CURVE('',#12956,#12957,#6456,.T.) ;
#16032=EDGE_CURVE('',#12957,#12958,#768,.T.) ;
#16033=EDGE_CURVE('',#12958,#12959,#769,.T.) ;
#16034=EDGE_CURVE('',#12960,#12959,#6457,.T.) ;
#16035=EDGE_CURVE('',#12954,#12960,#770,.T.) ;
#16036=EDGE_CURVE('',#12956,#12954,#771,.T.) ;
#16037=EDGE_CURVE('',#12959,#12961,#772,.T.) ;
#16038=EDGE_CURVE('',#12961,#12962,#773,.T.) ;
#16039=EDGE_CURVE('',#12963,#12962,#6458,.T.) ;
#16040=EDGE_CURVE('',#12955,#12963,#774,.T.) ;
#16041=EDGE_CURVE('',#12960,#12955,#775,.T.) ;
#16042=EDGE_CURVE('',#12962,#12947,#776,.T.) ;
#16043=EDGE_CURVE('',#12951,#12948,#6459,.T.) ;
#16044=EDGE_CURVE('',#12963,#12949,#777,.T.) ;
#16045=EDGE_CURVE('',#12946,#12964,#778,.T.) ;
#16046=EDGE_CURVE('',#12965,#12964,#6460,.T.) ;
#16047=EDGE_CURVE('',#12950,#12965,#779,.T.) ;
#16048=EDGE_CURVE('',#12964,#12966,#780,.T.) ;
#16049=EDGE_CURVE('',#12966,#12967,#781,.T.) ;
#16050=EDGE_CURVE('',#12968,#12967,#6461,.T.) ;
#16051=EDGE_CURVE('',#12952,#12968,#782,.T.) ;
#16052=EDGE_CURVE('',#12965,#12952,#783,.T.) ;
#16053=EDGE_CURVE('',#12967,#12969,#784,.T.) ;
#16054=EDGE_CURVE('',#12969,#12957,#785,.T.) ;
#16055=EDGE_CURVE('',#12953,#12956,#786,.T.) ;
#16056=EDGE_CURVE('',#12968,#12953,#787,.T.) ;
#16057=EDGE_CURVE('',#12947,#12961,#11046,.T.) ;
#16058=EDGE_CURVE('',#12961,#12958,#11047,.T.) ;
#16059=EDGE_CURVE('',#12958,#12969,#11048,.T.) ;
#16060=EDGE_CURVE('',#12969,#12966,#11049,.T.) ;
#16061=EDGE_CURVE('',#12946,#12966,#11050,.T.) ;
#21124=ORIENTED_EDGE('',*,*,#15968,.T.) ;
#21125=ORIENTED_EDGE('',*,*,#15969,.T.) ;
#21126=ORIENTED_EDGE('',*,*,#15970,.T.) ;
#21127=ORIENTED_EDGE('',*,*,#15971,.F.) ;
#21128=ORIENTED_EDGE('',*,*,#15972,.T.) ;
#21129=ORIENTED_EDGE('',*,*,#15973,.T.) ;
#21130=ORIENTED_EDGE('',*,*,#15968,.F.) ;
#21131=ORIENTED_EDGE('',*,*,#15974,.F.) ;
#21132=ORIENTED_EDGE('',*,*,#15975,.T.) ;
#21133=ORIENTED_EDGE('',*,*,#15976,.T.) ;
#21134=ORIENTED_EDGE('',*,*,#15972,.F.) ;
#21135=ORIENTED_EDGE('',*,*,#15977,.F.) ;
#21136=ORIENTED_EDGE('',*,*,#15978,.T.) ;
#21137=ORIENTED_EDGE('',*,*,#15979,.T.) ;
#21138=ORIENTED_EDGE('',*,*,#15975,.F.) ;
#21139=ORIENTED_EDGE('',*,*,#15980,.F.) ;
#21140=ORIENTED_EDGE('',*,*,#15981,.F.) ;
#21141=ORIENTED_EDGE('',*,*,#15982,.F.) ;
#21142=ORIENTED_EDGE('',*,*,#15983,.F.) ;
#21143=ORIENTED_EDGE('',*,*,#15984,.T.) ;
#21144=ORIENTED_EDGE('',*,*,#15985,.T.) ;
#21145=ORIENTED_EDGE('',*,*,#15986,.F.) ;
#21146=ORIENTED_EDGE('',*,*,#15987,.F.) ;
#21147=ORIENTED_EDGE('',*,*,#15988,.F.) ;
#21148=ORIENTED_EDGE('',*,*,#15989,.T.) ;
#21149=ORIENTED_EDGE('',*,*,#15990,.F.) ;
#21150=ORIENTED_EDGE('',*,*,#15985,.F.) ;
#21151=ORIENTED_EDGE('',*,*,#15991,.F.) ;
#21152=ORIENTED_EDGE('',*,*,#15992,.T.) ;
#21153=ORIENTED_EDGE('',*,*,#15993,.F.) ;
#21154=ORIENTED_EDGE('',*,*,#15989,.F.) ;
#21155=ORIENTED_EDGE('',*,*,#15994,.F.) ;
#21156=ORIENTED_EDGE('',*,*,#15995,.T.) ;
#21157=ORIENTED_EDGE('',*,*,#15996,.F.) ;
#21158=ORIENTED_EDGE('',*,*,#15992,.F.) ;
#21159=ORIENTED_EDGE('',*,*,#15997,.F.) ;
#21160=ORIENTED_EDGE('',*,*,#15998,.T.) ;
#21161=ORIENTED_EDGE('',*,*,#15999,.F.) ;
#21162=ORIENTED_EDGE('',*,*,#15995,.F.) ;
#21163=ORIENTED_EDGE('',*,*,#16000,.F.) ;
#21164=ORIENTED_EDGE('',*,*,#16001,.F.) ;
#21165=ORIENTED_EDGE('',*,*,#16002,.F.) ;
#21166=ORIENTED_EDGE('',*,*,#16003,.T.) ;
#21167=ORIENTED_EDGE('',*,*,#16004,.F.) ;
#21168=ORIENTED_EDGE('',*,*,#16005,.F.) ;
#21169=ORIENTED_EDGE('',*,*,#16006,.T.) ;
#21170=ORIENTED_EDGE('',*,*,#15983,.T.) ;
#21171=ORIENTED_EDGE('',*,*,#16007,.T.) ;
#21172=ORIENTED_EDGE('',*,*,#16008,.F.) ;
#21173=ORIENTED_EDGE('',*,*,#16009,.F.) ;
#21174=ORIENTED_EDGE('',*,*,#15970,.F.) ;
#21175=ORIENTED_EDGE('',*,*,#16010,.F.) ;
#21176=ORIENTED_EDGE('',*,*,#16008,.T.) ;
#21177=ORIENTED_EDGE('',*,*,#16011,.F.) ;
#21178=ORIENTED_EDGE('',*,*,#16012,.F.) ;
#21179=ORIENTED_EDGE('',*,*,#16005,.T.) ;
#21180=ORIENTED_EDGE('',*,*,#16013,.T.) ;
#21181=ORIENTED_EDGE('',*,*,#16014,.T.) ;
#21182=ORIENTED_EDGE('',*,*,#16015,.T.) ;
#21183=ORIENTED_EDGE('',*,*,#16001,.T.) ;
#21184=ORIENTED_EDGE('',*,*,#16016,.F.) ;
#21185=ORIENTED_EDGE('',*,*,#15998,.F.) ;
#21186=ORIENTED_EDGE('',*,*,#16017,.F.) ;
#21187=ORIENTED_EDGE('',*,*,#15981,.T.) ;
#21188=ORIENTED_EDGE('',*,*,#16018,.T.) ;
#21189=ORIENTED_EDGE('',*,*,#15978,.F.) ;
#21190=ORIENTED_EDGE('',*,*,#16019,.F.) ;
#21191=ORIENTED_EDGE('',*,*,#16020,.F.) ;
#21192=ORIENTED_EDGE('',*,*,#16021,.F.) ;
#21193=ORIENTED_EDGE('',*,*,#16022,.F.) ;
#21194=ORIENTED_EDGE('',*,*,#16023,.F.) ;
#21195=ORIENTED_EDGE('',*,*,#16024,.T.) ;
#21196=ORIENTED_EDGE('',*,*,#16025,.T.) ;
#21197=ORIENTED_EDGE('',*,*,#16002,.T.) ;
#21198=ORIENTED_EDGE('',*,*,#16017,.T.) ;
#21199=ORIENTED_EDGE('',*,*,#16000,.T.) ;
#21200=ORIENTED_EDGE('',*,*,#15997,.T.) ;
#21201=ORIENTED_EDGE('',*,*,#15994,.T.) ;
#21202=ORIENTED_EDGE('',*,*,#15991,.T.) ;
#21203=ORIENTED_EDGE('',*,*,#15988,.T.) ;
#21204=ORIENTED_EDGE('',*,*,#16010,.T.) ;
#21205=ORIENTED_EDGE('',*,*,#15969,.F.) ;
#21206=ORIENTED_EDGE('',*,*,#15973,.F.) ;
#21207=ORIENTED_EDGE('',*,*,#15976,.F.) ;
#21208=ORIENTED_EDGE('',*,*,#15979,.F.) ;
#21209=ORIENTED_EDGE('',*,*,#16018,.F.) ;
#21210=ORIENTED_EDGE('',*,*,#15984,.F.) ;
#21211=ORIENTED_EDGE('',*,*,#16006,.F.) ;
#21212=ORIENTED_EDGE('',*,*,#16015,.F.) ;
#21213=ORIENTED_EDGE('',*,*,#15982,.T.) ;
#21214=ORIENTED_EDGE('',*,*,#16019,.T.) ;
#21215=ORIENTED_EDGE('',*,*,#15980,.T.) ;
#21216=ORIENTED_EDGE('',*,*,#15977,.T.) ;
#21217=ORIENTED_EDGE('',*,*,#15974,.T.) ;
#21218=ORIENTED_EDGE('',*,*,#15971,.T.) ;
#21219=ORIENTED_EDGE('',*,*,#16009,.T.) ;
#21220=ORIENTED_EDGE('',*,*,#16012,.T.) ;
#21221=ORIENTED_EDGE('',*,*,#15986,.T.) ;
#21222=ORIENTED_EDGE('',*,*,#15990,.T.) ;
#21223=ORIENTED_EDGE('',*,*,#15993,.T.) ;
#21224=ORIENTED_EDGE('',*,*,#15996,.T.) ;
#21225=ORIENTED_EDGE('',*,*,#15999,.T.) ;
#21226=ORIENTED_EDGE('',*,*,#16016,.T.) ;
#21227=ORIENTED_EDGE('',*,*,#16004,.T.) ;
#21228=ORIENTED_EDGE('',*,*,#16013,.F.) ;
#21229=ORIENTED_EDGE('',*,*,#16007,.F.) ;
#21230=ORIENTED_EDGE('',*,*,#16023,.T.) ;
#21231=ORIENTED_EDGE('',*,*,#16026,.T.) ;
#21232=ORIENTED_EDGE('',*,*,#16027,.T.) ;
#21233=ORIENTED_EDGE('',*,*,#16028,.T.) ;
#21234=ORIENTED_EDGE('',*,*,#16029,.T.) ;
#21235=ORIENTED_EDGE('',*,*,#16030,.T.) ;
#21236=ORIENTED_EDGE('',*,*,#16014,.F.) ;
#21237=ORIENTED_EDGE('',*,*,#16003,.F.) ;
#21238=ORIENTED_EDGE('',*,*,#16031,.T.) ;
#21239=ORIENTED_EDGE('',*,*,#16032,.T.) ;
#21240=ORIENTED_EDGE('',*,*,#16033,.T.) ;
#21241=ORIENTED_EDGE('',*,*,#16034,.F.) ;
#21242=ORIENTED_EDGE('',*,*,#16035,.F.) ;
#21243=ORIENTED_EDGE('',*,*,#16036,.F.) ;
#21244=ORIENTED_EDGE('',*,*,#16034,.T.) ;
#21245=ORIENTED_EDGE('',*,*,#16037,.T.) ;
#21246=ORIENTED_EDGE('',*,*,#16038,.T.) ;
#21247=ORIENTED_EDGE('',*,*,#16039,.F.) ;
#21248=ORIENTED_EDGE('',*,*,#16040,.F.) ;
#21249=ORIENTED_EDGE('',*,*,#16041,.F.) ;
#21250=ORIENTED_EDGE('',*,*,#16039,.T.) ;
#21251=ORIENTED_EDGE('',*,*,#16042,.T.) ;
#21252=ORIENTED_EDGE('',*,*,#16022,.T.) ;
#21253=ORIENTED_EDGE('',*,*,#16043,.F.) ;
#21254=ORIENTED_EDGE('',*,*,#16024,.F.) ;
#21255=ORIENTED_EDGE('',*,*,#16044,.F.) ;
#21256=ORIENTED_EDGE('',*,*,#16043,.T.) ;
#21257=ORIENTED_EDGE('',*,*,#16021,.T.) ;
#21258=ORIENTED_EDGE('',*,*,#16045,.T.) ;
#21259=ORIENTED_EDGE('',*,*,#16046,.F.) ;
#21260=ORIENTED_EDGE('',*,*,#16047,.F.) ;
#21261=ORIENTED_EDGE('',*,*,#16025,.F.) ;
#21262=ORIENTED_EDGE('',*,*,#16046,.T.) ;
#21263=ORIENTED_EDGE('',*,*,#16048,.T.) ;
#21264=ORIENTED_EDGE('',*,*,#16049,.T.) ;
#21265=ORIENTED_EDGE('',*,*,#16050,.F.) ;
#21266=ORIENTED_EDGE('',*,*,#16051,.F.) ;
#21267=ORIENTED_EDGE('',*,*,#16052,.F.) ;
#21268=ORIENTED_EDGE('',*,*,#16050,.T.) ;
#21269=ORIENTED_EDGE('',*,*,#16053,.T.) ;
#21270=ORIENTED_EDGE('',*,*,#16054,.T.) ;
#21271=ORIENTED_EDGE('',*,*,#16031,.F.) ;
#21272=ORIENTED_EDGE('',*,*,#16055,.F.) ;
#21273=ORIENTED_EDGE('',*,*,#16056,.F.) ;
#21274=ORIENTED_EDGE('',*,*,#16020,.T.) ;
#21275=ORIENTED_EDGE('',*,*,#16057,.T.) ;
#21276=ORIENTED_EDGE('',*,*,#16058,.T.) ;
#21277=ORIENTED_EDGE('',*,*,#16059,.T.) ;
#21278=ORIENTED_EDGE('',*,*,#16060,.T.) ;
#21279=ORIENTED_EDGE('',*,*,#16061,.F.) ;
#21280=ORIENTED_EDGE('',*,*,#15987,.T.) ;
#21281=ORIENTED_EDGE('',*,*,#16011,.T.) ;
#21282=ORIENTED_EDGE('',*,*,#16036,.T.) ;
#21283=ORIENTED_EDGE('',*,*,#16028,.F.) ;
#21284=ORIENTED_EDGE('',*,*,#16055,.T.) ;
#21285=ORIENTED_EDGE('',*,*,#16051,.T.) ;
#21286=ORIENTED_EDGE('',*,*,#16056,.T.) ;
#21287=ORIENTED_EDGE('',*,*,#16027,.F.) ;
#21288=ORIENTED_EDGE('',*,*,#16047,.T.) ;
#21289=ORIENTED_EDGE('',*,*,#16052,.T.) ;
#21290=ORIENTED_EDGE('',*,*,#16026,.F.) ;
#21291=ORIENTED_EDGE('',*,*,#16040,.T.) ;
#21292=ORIENTED_EDGE('',*,*,#16044,.T.) ;
#21293=ORIENTED_EDGE('',*,*,#16030,.F.) ;
#21294=ORIENTED_EDGE('',*,*,#16035,.T.) ;
#21295=ORIENTED_EDGE('',*,*,#16041,.T.) ;
#21296=ORIENTED_EDGE('',*,*,#16029,.F.) ;
#21297=ORIENTED_EDGE('',*,*,#16061,.T.) ;
#21298=ORIENTED_EDGE('',*,*,#16048,.F.) ;
#21299=ORIENTED_EDGE('',*,*,#16045,.F.) ;
#21300=ORIENTED_EDGE('',*,*,#16060,.F.) ;
#21301=ORIENTED_EDGE('',*,*,#16053,.F.) ;
#21302=ORIENTED_EDGE('',*,*,#16049,.F.) ;
#21303=ORIENTED_EDGE('',*,*,#16054,.F.) ;
#21304=ORIENTED_EDGE('',*,*,#16059,.F.) ;
#21305=ORIENTED_EDGE('',*,*,#16032,.F.) ;
#21306=ORIENTED_EDGE('',*,*,#16058,.F.) ;
#21307=ORIENTED_EDGE('',*,*,#16037,.F.) ;
#21308=ORIENTED_EDGE('',*,*,#16033,.F.) ;
#21309=ORIENTED_EDGE('',*,*,#16057,.F.) ;
#21310=ORIENTED_EDGE('',*,*,#16042,.F.) ;
#21311=ORIENTED_EDGE('',*,*,#16038,.F.) ;
#30026=CYLINDRICAL_SURFACE('',#33063,1.17524047358083) ;
#30027=CYLINDRICAL_SURFACE('',#33065,1.17524047358083) ;
#30028=CYLINDRICAL_SURFACE('',#33066,1.17524047358083) ;
#30029=CYLINDRICAL_SURFACE('',#33067,1.17524047358083) ;
#30030=CYLINDRICAL_SURFACE('',#33068,1.17524047358083) ;
#30031=CYLINDRICAL_SURFACE('',#33070,1.5) ;
#30032=CYLINDRICAL_SURFACE('',#33072,1.5) ;
#30033=CYLINDRICAL_SURFACE('',#33073,1.5) ;
#30034=CYLINDRICAL_SURFACE('',#33074,1.5) ;
#30035=CYLINDRICAL_SURFACE('',#33075,1.5) ;
#30036=CYLINDRICAL_SURFACE('',#33076,1.5) ;
#30037=CYLINDRICAL_SURFACE('',#33084,1.5) ;
#30038=CYLINDRICAL_SURFACE('',#33085,1.17524047358083) ;
#30877=ADVANCED_FACE('',(#2398),#30026,.F.) ;
#30878=ADVANCED_FACE('',(#2399),#30027,.F.) ;
#30879=ADVANCED_FACE('',(#2400),#30028,.F.) ;
#30880=ADVANCED_FACE('',(#2401),#30029,.F.) ;
#30881=ADVANCED_FACE('',(#2402),#30030,.F.) ;
#30882=ADVANCED_FACE('',(#2403),#30031,.F.) ;
#30883=ADVANCED_FACE('',(#2404),#30032,.F.) ;
#30884=ADVANCED_FACE('',(#2405),#30033,.F.) ;
#30885=ADVANCED_FACE('',(#2406),#30034,.F.) ;
#30886=ADVANCED_FACE('',(#2407),#30035,.F.) ;
#30887=ADVANCED_FACE('',(#2408),#30036,.F.) ;
#30888=ADVANCED_FACE('',(#2409),#864,.F.) ;
#30889=ADVANCED_FACE('',(#2410),#865,.F.) ;
#30890=ADVANCED_FACE('',(#2411),#866,.F.) ;
#30891=ADVANCED_FACE('',(#2412),#867,.F.) ;
#30892=ADVANCED_FACE('',(#2413),#30037,.F.) ;
#30893=ADVANCED_FACE('',(#2414),#30038,.F.) ;
#30894=ADVANCED_FACE('',(#2415),#868,.T.) ;
#30895=ADVANCED_FACE('',(#2416),#869,.T.) ;
#30896=ADVANCED_FACE('',(#2417),#736,.T.) ;
#30897=ADVANCED_FACE('',(#2418),#737,.T.) ;
#30898=ADVANCED_FACE('',(#2419,#1048),#1752,.T.) ;
#30899=ADVANCED_FACE('',(#2420),#1753,.F.) ;
#30900=ADVANCED_FACE('',(#2421),#1754,.F.) ;
#30901=ADVANCED_FACE('',(#2422),#1755,.F.) ;
#30902=ADVANCED_FACE('',(#2423),#1756,.F.) ;
#30903=ADVANCED_FACE('',(#2424),#1757,.F.) ;
#30904=ADVANCED_FACE('',(#2425),#1758,.F.) ;
#30905=ADVANCED_FACE('',(#2426,#1049),#1759,.F.) ;
#30906=ADVANCED_FACE('',(#2427),#870,.T.) ;
#30907=ADVANCED_FACE('',(#2428),#871,.T.) ;
#30908=ADVANCED_FACE('',(#2429),#872,.T.) ;
#30909=ADVANCED_FACE('',(#2430),#873,.T.) ;
#30910=ADVANCED_FACE('',(#2431),#874,.T.) ;
#30911=ADVANCED_FACE('',(#2432),#875,.T.) ;
#30912=ADVANCED_FACE('',(#2433),#876,.T.) ;
#30913=ADVANCED_FACE('',(#2434),#877,.T.) ;
#30914=ADVANCED_FACE('',(#2435),#878,.T.) ;
#30915=ADVANCED_FACE('',(#2436),#879,.T.) ;
#32638=CLOSED_SHELL('',(#30877,#30878,#30879,#30880,#30881,#30882,#30883,
#30884,#30885,#30886,#30887,#30888,#30889,#30890,#30891,#30892,#30893,#30894,
#30895,#30896,#30897,#30898,#30899,#30900,#30901,#30902,#30903,#30904,#30905,
#30906,#30907,#30908,#30909,#30910,#30911,#30912,#30913,#30914,#30915)) ;
#33062=AXIS2_PLACEMENT_3D('',#47175,#37313,#37314) ;
#33063=AXIS2_PLACEMENT_3D('',#47176,#37315,#37316) ;
#33064=AXIS2_PLACEMENT_3D('',#47192,#37318,#37319) ;
#33065=AXIS2_PLACEMENT_3D('',#47207,#37320,#37321) ;
#33066=AXIS2_PLACEMENT_3D('',#47283,#37323,#37324) ;
#33067=AXIS2_PLACEMENT_3D('',#47361,#37326,#37327) ;
#33068=AXIS2_PLACEMENT_3D('',#47439,#37329,#37330) ;
#33069=AXIS2_PLACEMENT_3D('',#47459,#37332,#37333) ;
#33070=AXIS2_PLACEMENT_3D('',#47478,#37334,#37335) ;
#33071=AXIS2_PLACEMENT_3D('',#47500,#37337,#37338) ;
#33072=AXIS2_PLACEMENT_3D('',#47521,#37339,#37340) ;
#33073=AXIS2_PLACEMENT_3D('',#47597,#37342,#37343) ;
#33074=AXIS2_PLACEMENT_3D('',#47673,#37345,#37346) ;
#33075=AXIS2_PLACEMENT_3D('',#47753,#37348,#37349) ;
#33076=AXIS2_PLACEMENT_3D('',#47829,#37351,#37352) ;
#33077=AXIS2_PLACEMENT_3D('',#47855,#37354,#37355) ;
#33078=AXIS2_PLACEMENT_3D('',#47880,#37356,#37357) ;
#33079=AXIS2_PLACEMENT_3D('',#47896,#37359,#37360) ;
#33080=AXIS2_PLACEMENT_3D('',#47921,#37362,#37363) ;
#33081=AXIS2_PLACEMENT_3D('',#47922,#37364,#37365) ;
#33082=AXIS2_PLACEMENT_3D('',#47959,#37366,#37367) ;
#33083=AXIS2_PLACEMENT_3D('',#47968,#37368,#37369) ;
#33084=AXIS2_PLACEMENT_3D('',#48009,#37370,#37371) ;
#33085=AXIS2_PLACEMENT_3D('',#48082,#37372,#37373) ;
#33086=AXIS2_PLACEMENT_3D('',#48155,#37374,#37375) ;
#33087=AXIS2_PLACEMENT_3D('',#48158,#37376,#37377) ;
#33088=AXIS2_PLACEMENT_3D('',#48166,#37378,#37379) ;
#33089=AXIS2_PLACEMENT_3D('',#48169,#37380,#37381) ;
#33090=AXIS2_PLACEMENT_3D('',#48517,#37382,#37383) ;
#33091=AXIS2_PLACEMENT_3D('',#48519,#37384,#37385) ;
#33092=AXIS2_PLACEMENT_3D('',#48521,#37386,#37387) ;
#33093=AXIS2_PLACEMENT_3D('',#48523,#37388,#37389) ;
#33094=AXIS2_PLACEMENT_3D('',#48525,#37390,#37391) ;
#33095=AXIS2_PLACEMENT_3D('',#48526,#37392,#37393) ;
#33096=AXIS2_PLACEMENT_3D('',#48527,#37394,#37395) ;
#33097=AXIS2_PLACEMENT_3D('',#48547,#37398,#37399) ;
#33098=AXIS2_PLACEMENT_3D('',#48564,#37401,#37402) ;
#33099=AXIS2_PLACEMENT_3D('',#48572,#37404,#37405) ;
#33100=AXIS2_PLACEMENT_3D('',#48582,#37407,#37408) ;
#33101=AXIS2_PLACEMENT_3D('',#48599,#37410,#37411) ;
#33102=AXIS2_PLACEMENT_3D('',#48613,#37412,#37413) ;
#33103=AXIS2_PLACEMENT_3D('',#48614,#37414,#37415) ;
#33104=AXIS2_PLACEMENT_3D('',#48615,#37416,#37417) ;
#33105=AXIS2_PLACEMENT_3D('',#48616,#37418,#37419) ;
#33106=AXIS2_PLACEMENT_3D('',#48617,#37420,#37421) ;
#33107=AXIS2_PLACEMENT_3D('',#48618,#37422,#37423) ;
#33108=AXIS2_PLACEMENT_3D('',#48619,#37424,#37425) ;
#33109=AXIS2_PLACEMENT_3D('',#48620,#37426,#37427) ;
#33110=AXIS2_PLACEMENT_3D('',#48621,#37428,#37429) ;
#33111=AXIS2_PLACEMENT_3D('',#48622,#37430,#37431) ;
#33112=AXIS2_PLACEMENT_3D('',#48623,#37432,#37433) ;
#33113=AXIS2_PLACEMENT_3D('',#48624,#37434,#37435) ;
#33114=AXIS2_PLACEMENT_3D('',#48625,#37436,#37437) ;
#33115=AXIS2_PLACEMENT_3D('',#48626,#37438,#37439) ;
#33116=AXIS2_PLACEMENT_3D('',#48627,#37440,#37441) ;
#33117=AXIS2_PLACEMENT_3D('',#48628,#37442,#37443) ;
#37313=DIRECTION('axis',(0.,0.,1.)) ;
#37314=DIRECTION('refdir',(1.,0.,0.)) ;
#37315=DIRECTION('center_axis',(0.,-1.,0.)) ;
#37316=DIRECTION('ref_axis',(-2.9521166348046E-16,0.,-1.)) ;
#37317=DIRECTION('',(0.,-1.,0.)) ;
#37318=DIRECTION('center_axis',(-7.50335137235545E-15,-1.,-1.88069991130403E-15)) ;
#37319=DIRECTION('ref_axis',(-0.802795663530002,7.14503324610129E-15,-0.596254243269953)) ;
#37320=DIRECTION('center_axis',(0.,-1.,0.)) ;
#37321=DIRECTION('ref_axis',(-2.9521166348046E-16,0.,-1.)) ;
#37322=DIRECTION('',(0.,-1.,0.)) ;
#37323=DIRECTION('center_axis',(0.,-1.,0.)) ;
#37324=DIRECTION('ref_axis',(-2.9521166348046E-16,0.,-1.)) ;
#37325=DIRECTION('',(0.,-1.,0.)) ;
#37326=DIRECTION('center_axis',(0.,-1.,0.)) ;
#37327=DIRECTION('ref_axis',(-2.9521166348046E-16,0.,-1.)) ;
#37328=DIRECTION('',(0.,-1.,0.)) ;
#37329=DIRECTION('center_axis',(0.,-1.,0.)) ;
#37330=DIRECTION('ref_axis',(-2.9521166348046E-16,0.,-1.)) ;
#37331=DIRECTION('',(0.,-1.,0.)) ;
#37332=DIRECTION('center_axis',(8.41776735018431E-16,-1.,-1.3808398081996E-15)) ;
#37333=DIRECTION('ref_axis',(0.802795663530003,1.49910630744832E-15,-0.596254243269952)) ;
#37334=DIRECTION('center_axis',(0.,-1.,0.)) ;
#37335=DIRECTION('ref_axis',(0.,0.,-1.)) ;
#37336=DIRECTION('',(0.,-1.,0.)) ;
#37337=DIRECTION('center_axis',(0.,1.,0.)) ;
#37338=DIRECTION('ref_axis',(0.,0.,1.)) ;
#37339=DIRECTION('center_axis',(0.,-1.,0.)) ;
#37340=DIRECTION('ref_axis',(0.,0.,-1.)) ;
#37341=DIRECTION('',(0.,-1.,0.)) ;
#37342=DIRECTION('center_axis',(0.,-1.,0.)) ;
#37343=DIRECTION('ref_axis',(0.,0.,-1.)) ;
#37344=DIRECTION('',(0.,-1.,0.)) ;
#37345=DIRECTION('center_axis',(0.,-1.,0.)) ;
#37346=DIRECTION('ref_axis',(0.,0.,-1.)) ;
#37347=DIRECTION('',(0.,-1.,0.)) ;
#37348=DIRECTION('center_axis',(0.,-1.,0.)) ;
#37349=DIRECTION('ref_axis',(0.,0.,-1.)) ;
#37350=DIRECTION('',(0.,-1.,0.)) ;
#37351=DIRECTION('center_axis',(0.,-1.,0.)) ;
#37352=DIRECTION('ref_axis',(0.,0.,-1.)) ;
#37353=DIRECTION('',(0.,-1.,0.)) ;
#37354=DIRECTION('center_axis',(0.,1.,0.)) ;
#37355=DIRECTION('ref_axis',(0.,0.,1.)) ;
#37356=DIRECTION('center_axis',(0.,1.,0.)) ;
#37357=DIRECTION('ref_axis',(0.,0.,1.)) ;
#37358=DIRECTION('',(-8.65956056235495E-17,0.707106781186546,-0.707106781186549)) ;
#37359=DIRECTION('center_axis',(0.,-1.,0.)) ;
#37360=DIRECTION('ref_axis',(0.,0.,1.)) ;
#37361=DIRECTION('',(8.65956056235495E-17,-0.707106781186546,-0.707106781186549)) ;
#37362=DIRECTION('center_axis',(0.,-1.,0.)) ;
#37363=DIRECTION('ref_axis',(0.,0.,1.)) ;
#37364=DIRECTION('center_axis',(0.,1.,0.)) ;
#37365=DIRECTION('ref_axis',(0.,0.,1.)) ;
#37366=DIRECTION('center_axis',(0.,1.,0.)) ;
#37367=DIRECTION('ref_axis',(0.,0.,1.)) ;
#37368=DIRECTION('center_axis',(0.,1.,0.)) ;
#37369=DIRECTION('ref_axis',(0.,0.,1.)) ;
#37370=DIRECTION('center_axis',(0.,-1.,0.)) ;
#37371=DIRECTION('ref_axis',(0.,0.,-1.)) ;
#37372=DIRECTION('center_axis',(0.,-1.,0.)) ;
#37373=DIRECTION('ref_axis',(-2.9521166348046E-16,0.,-1.)) ;
#37374=DIRECTION('center_axis',(0.,1.,0.)) ;
#37375=DIRECTION('ref_axis',(0.,0.,1.)) ;
#37376=DIRECTION('center_axis',(0.,-1.,0.)) ;
#37377=DIRECTION('ref_axis',(0.,0.,1.)) ;
#37378=DIRECTION('center_axis',(0.,-1.,0.)) ;
#37379=DIRECTION('ref_axis',(0.,0.,1.)) ;
#37380=DIRECTION('center_axis',(0.,1.,0.)) ;
#37381=DIRECTION('ref_axis',(0.,0.,1.)) ;
#37382=DIRECTION('center_axis',(0.,1.,0.)) ;
#37383=DIRECTION('ref_axis',(0.,0.,1.)) ;
#37384=DIRECTION('center_axis',(0.,1.,0.)) ;
#37385=DIRECTION('ref_axis',(0.,0.,1.)) ;
#37386=DIRECTION('center_axis',(0.,1.,0.)) ;
#37387=DIRECTION('ref_axis',(0.,0.,1.)) ;
#37388=DIRECTION('center_axis',(0.,1.,0.)) ;
#37389=DIRECTION('ref_axis',(0.,0.,1.)) ;
#37390=DIRECTION('center_axis',(0.,1.,0.)) ;
#37391=DIRECTION('ref_axis',(0.,0.,1.)) ;
#37392=DIRECTION('center_axis',(0.,1.,0.)) ;
#37393=DIRECTION('ref_axis',(0.,0.,1.)) ;
#37394=DIRECTION('center_axis',(0.5,0.,0.866025403784439)) ;
#37395=DIRECTION('ref_axis',(0.866025403784439,0.,-0.5)) ;
#37396=DIRECTION('',(0.,-1.,0.)) ;
#37397=DIRECTION('',(0.,-1.,0.)) ;
#37398=DIRECTION('center_axis',(1.,0.,-1.36574054430651E-16)) ;
#37399=DIRECTION('ref_axis',(-1.36574054430651E-16,0.,-1.)) ;
#37400=DIRECTION('',(0.,-1.,0.)) ;
#37401=DIRECTION('center_axis',(0.5,0.,-0.866025403784439)) ;
#37402=DIRECTION('ref_axis',(-0.866025403784439,0.,-0.5)) ;
#37403=DIRECTION('',(0.,-1.,0.)) ;
#37404=DIRECTION('center_axis',(-0.5,0.,-0.866025403784438)) ;
#37405=DIRECTION('ref_axis',(-0.866025403784438,0.,0.5)) ;
#37406=DIRECTION('',(0.,-1.,0.)) ;
#37407=DIRECTION('center_axis',(-1.,0.,0.)) ;
#37408=DIRECTION('ref_axis',(0.,0.,1.)) ;
#37409=DIRECTION('',(0.,-1.,0.)) ;
#37410=DIRECTION('center_axis',(-0.5,0.,0.866025403784439)) ;
#37411=DIRECTION('ref_axis',(0.866025403784439,0.,0.5)) ;
#37412=DIRECTION('center_axis',(0.,1.,0.)) ;
#37413=DIRECTION('ref_axis',(0.,0.,1.)) ;
#37414=DIRECTION('center_axis',(0.,-1.,0.)) ;
#37415=DIRECTION('ref_axis',(0.,0.,1.)) ;
#37416=DIRECTION('center_axis',(0.,-1.,0.)) ;
#37417=DIRECTION('ref_axis',(0.,0.,1.)) ;
#37418=DIRECTION('center_axis',(0.,-1.,0.)) ;
#37419=DIRECTION('ref_axis',(1.77635683940025E-15,0.,1.)) ;
#37420=DIRECTION('center_axis',(0.,-1.,0.)) ;
#37421=DIRECTION('ref_axis',(0.,0.,1.)) ;
#37422=DIRECTION('center_axis',(0.,1.,0.)) ;
#37423=DIRECTION('ref_axis',(0.,0.,1.)) ;
#37424=DIRECTION('center_axis',(0.,-1.,0.)) ;
#37425=DIRECTION('ref_axis',(-1.01064309961486E-15,0.,-1.)) ;
#37426=DIRECTION('center_axis',(0.,-1.,0.)) ;
#37427=DIRECTION('ref_axis',(0.,0.,1.)) ;
#37428=DIRECTION('center_axis',(0.,-1.,0.)) ;
#37429=DIRECTION('ref_axis',(0.,0.,1.)) ;
#37430=DIRECTION('center_axis',(0.,-1.,0.)) ;
#37431=DIRECTION('ref_axis',(0.,0.,1.)) ;
#37432=DIRECTION('center_axis',(0.,-1.,0.)) ;
#37433=DIRECTION('ref_axis',(0.,0.,1.)) ;
#37434=DIRECTION('center_axis',(0.,1.,0.)) ;
#37435=DIRECTION('ref_axis',(0.,0.,1.)) ;
#37436=DIRECTION('center_axis',(0.,1.,0.)) ;
#37437=DIRECTION('ref_axis',(0.,0.,1.)) ;
#37438=DIRECTION('center_axis',(0.,1.,0.)) ;
#37439=DIRECTION('ref_axis',(1.22464679914735E-16,0.,-1.)) ;
#37440=DIRECTION('center_axis',(0.,1.,0.)) ;
#37441=DIRECTION('ref_axis',(0.,0.,1.)) ;
#37442=DIRECTION('center_axis',(0.,1.,0.)) ;
#37443=DIRECTION('ref_axis',(0.,0.,1.)) ;
#47175=CARTESIAN_POINT('',(0.,0.,0.)) ;
#47176=CARTESIAN_POINT('Origin',(3.46944695195362E-16,1.71875,2.77555756156289E-16)) ;
#47177=CARTESIAN_POINT('',(2.68827523286988E-13,-0.999999999999967,1.17524047358083)) ;
#47178=CARTESIAN_POINT('',(2.03174352947591E-13,-1.06249999999997,1.17524047358083)) ;
#47179=CARTESIAN_POINT('',(5.49963941970804E-16,1.71875,1.17524047358083)) ;
#47180=CARTESIAN_POINT('',(-1.16245326511946,-1.17524047358083,0.172894699616842)) ;
#47181=CARTESIAN_POINT('Ctrl Pts',(4.05798741953211E-13,-1.06249999999997,
1.17524047358083)) ;
#47182=CARTESIAN_POINT('Ctrl Pts',(-0.105160340523186,-1.06895765188846,
1.17524047358083)) ;
#47183=CARTESIAN_POINT('Ctrl Pts',(-0.210026376843711,-1.07589739920494,
1.16113285033081)) ;
#47184=CARTESIAN_POINT('Ctrl Pts',(-0.461547030634828,-1.09379678097625,
1.09191353201678)) ;
#47185=CARTESIAN_POINT('Ctrl Pts',(-0.601609669732423,-1.10489587260588,
1.02145069830121)) ;
#47186=CARTESIAN_POINT('Ctrl Pts',(-0.841642087198107,-1.1262899253027,
0.833763281857878)) ;
#47187=CARTESIAN_POINT('Ctrl Pts',(-0.94076791668668,-1.13640781439979,
0.72007138829596)) ;
#47188=CARTESIAN_POINT('Ctrl Pts',(-1.09077083296657,-1.15476396114588,
0.462134782296477)) ;
#47189=CARTESIAN_POINT('Ctrl Pts',(-1.14052623621597,-1.16478687965435,
0.32032053973826)) ;
#47190=CARTESIAN_POINT('Ctrl Pts',(-1.16245326511978,-1.17524047358099,
0.172894699614671)) ;
#47191=CARTESIAN_POINT('',(-0.943477955795636,-1.17524047358083,-0.700742119235164)) ;
#47192=CARTESIAN_POINT('Origin',(8.46545056276682E-15,-1.17524047358084,
1.90819582357449E-15)) ;
#47193=CARTESIAN_POINT('Ctrl Pts',(-0.943477955795635,-1.17524047358084,
-0.700742119235159)) ;
#47194=CARTESIAN_POINT('Ctrl Pts',(-1.02492263848393,-1.16635139543542,
-0.591085141833767)) ;
#47195=CARTESIAN_POINT('Ctrl Pts',(-1.08661800606201,-1.15819168045143,
-0.468098475031939)) ;
#47196=CARTESIAN_POINT('Ctrl Pts',(-1.16970670338323,-1.13852263168986,
-0.190708128854841)) ;
#47197=CARTESIAN_POINT('Ctrl Pts',(-1.1845688827545,-1.12762622677339,-0.0370373759624758)) ;
#47198=CARTESIAN_POINT('Ctrl Pts',(-1.15431629966392,-1.10583767984718,
0.270244010535864)) ;
#47199=CARTESIAN_POINT('Ctrl Pts',(-1.10834405084586,-1.09516180730449,
0.420804620571442)) ;
#47200=CARTESIAN_POINT('Ctrl Pts',(-0.963542949730392,-1.07613113704493,
0.689191987712228)) ;
#47201=CARTESIAN_POINT('Ctrl Pts',(-0.868446230221078,-1.06642890978637,
0.8057548264429)) ;
#47202=CARTESIAN_POINT('Ctrl Pts',(-0.635333585436618,-1.04520090824001,
1.00074403996173)) ;
#47203=CARTESIAN_POINT('Ctrl Pts',(-0.498182457666835,-1.03412422046949,
1.07561784109633)) ;
#47204=CARTESIAN_POINT('Ctrl Pts',(-0.236805129209574,-1.01517846693789,
1.15727862072953)) ;
#47205=CARTESIAN_POINT('Ctrl Pts',(-0.118658074201543,-1.00728651631539,
1.17524047358083)) ;
#47206=CARTESIAN_POINT('Ctrl Pts',(5.37157124336218E-13,-0.999999999999967,
1.17524047358083)) ;
#47207=CARTESIAN_POINT('Origin',(3.46944695195362E-16,1.71875,2.77555756156289E-16)) ;
#47208=CARTESIAN_POINT('',(6.06086644654604E-14,-0.499999999999992,1.17524047358083)) ;
#47209=CARTESIAN_POINT('',(2.08586854750403E-13,-0.562499999999971,1.17524047358083)) ;
#47210=CARTESIAN_POINT('',(5.49963941970804E-16,1.71875,1.17524047358083)) ;
#47211=CARTESIAN_POINT('Ctrl Pts',(4.16923440216266E-13,-0.562499999999972,
1.17524047358083)) ;
#47212=CARTESIAN_POINT('Ctrl Pts',(-0.127484578485998,-0.570328531411307,
1.17524047358083)) ;
#47213=CARTESIAN_POINT('Ctrl Pts',(-0.254283442227845,-0.578850073610016,
1.15450587698244)) ;
#47214=CARTESIAN_POINT('Ctrl Pts',(-0.5217889700627,-0.598474486389227,
1.06431734245669)) ;
#47215=CARTESIAN_POINT('Ctrl Pts',(-0.656966876910855,-0.609529920381951,
0.986625301628538)) ;
#47216=CARTESIAN_POINT('Ctrl Pts',(-0.885467738610519,-0.630639702939782,
0.786982703254743)) ;
#47217=CARTESIAN_POINT('Ctrl Pts',(-0.977970250751646,-0.640095776533645,
0.668536344435955)) ;
#47218=CARTESIAN_POINT('Ctrl Pts',(-1.11701382207316,-0.659333626638224,
0.397227143624959)) ;
#47219=CARTESIAN_POINT('Ctrl Pts',(-1.15979113888618,-0.670077776473707,
0.245703626734443)) ;
#47220=CARTESIAN_POINT('Ctrl Pts',(-1.18349158051387,-0.691886539798171,
-0.0618628693174395)) ;
#47221=CARTESIAN_POINT('Ctrl Pts',(-1.1654693373561,-0.702736099361235,
-0.214872967545919)) ;
#47222=CARTESIAN_POINT('Ctrl Pts',(-1.07274162977296,-0.723158461972726,
-0.502887212831953)) ;
#47223=CARTESIAN_POINT('Ctrl Pts',(-0.999931264413838,-0.731959214886923,
-0.635457257089622)) ;
#47224=CARTESIAN_POINT('Ctrl Pts',(-0.803974158692238,-0.752358883134125,
-0.871437972397242)) ;
#47225=CARTESIAN_POINT('Ctrl Pts',(-0.680675739361065,-0.763452971793481,
-0.970796173861973)) ;
#47226=CARTESIAN_POINT('Ctrl Pts',(-0.40768984714355,-0.785241465149558,
-1.11253200080152)) ;
#47227=CARTESIAN_POINT('Ctrl Pts',(-0.261667978082255,-0.795736410110075,
-1.15563272262566)) ;
#47228=CARTESIAN_POINT('Ctrl Pts',(0.0417334207484942,-0.815392380307785,
-1.18453788613565)) ;
#47229=CARTESIAN_POINT('Ctrl Pts',(0.196297491712523,-0.824778579904694,
-1.16891088513489)) ;
#47230=CARTESIAN_POINT('Ctrl Pts',(0.491595152909961,-0.846111929617692,
-1.07865785321067)) ;
#47231=CARTESIAN_POINT('Ctrl Pts',(0.62928314668341,-0.857193583476491,
-1.00457385892074)) ;
#47232=CARTESIAN_POINT('Ctrl Pts',(0.863670959414044,-0.87845389091461,
-0.810882088475935)) ;
#47233=CARTESIAN_POINT('Ctrl Pts',(0.959488170589128,-0.888230928035835,
-0.694836089616553)) ;
#47234=CARTESIAN_POINT('Ctrl Pts',(1.10587053390409,-0.907204032554159,
-0.4272605655436)) ;
#47235=CARTESIAN_POINT('Ctrl Pts',(1.15271823191445,-0.917860247976333,
-0.276977177631598)) ;
#47236=CARTESIAN_POINT('Ctrl Pts',(1.18477406093944,-0.93964147802051,0.0302010197158971)) ;
#47237=CARTESIAN_POINT('Ctrl Pts',(1.17078511730657,-0.950549976117892,
0.18404232135617)) ;
#47238=CARTESIAN_POINT('Ctrl Pts',(1.08561597823129,-0.971132107238879,
0.474309763667351)) ;
#47239=CARTESIAN_POINT('Ctrl Pts',(1.01658369044885,-0.979975436753446,
0.608346112577959)) ;
#47240=CARTESIAN_POINT('Ctrl Pts',(0.82715575640286,-1.00015916197285,0.849544845288862)) ;
#47241=CARTESIAN_POINT('Ctrl Pts',(0.706221498175738,-1.01123358263976,
0.9524431430051)) ;
#47242=CARTESIAN_POINT('Ctrl Pts',(0.436336729474218,-1.03309702358497,
1.10166422799825)) ;
#47243=CARTESIAN_POINT('Ctrl Pts',(0.291099603261814,-1.04368051403565,
1.14862165815867)) ;
#47244=CARTESIAN_POINT('Ctrl Pts',(0.0940702185782331,-1.0566233702501,
1.17241999650976)) ;
#47245=CARTESIAN_POINT('Ctrl Pts',(0.0470118755424141,-1.05961311008155,
1.17524047358083)) ;
#47246=CARTESIAN_POINT('Ctrl Pts',(4.05798741953211E-13,-1.06249999999997,
1.17524047358083)) ;
#47247=CARTESIAN_POINT('Ctrl Pts',(5.37105082632005E-13,-0.999999999999967,
1.17524047358083)) ;
#47248=CARTESIAN_POINT('Ctrl Pts',(0.034994624013179,-0.997851061543523,
1.17524047358083)) ;
#47249=CARTESIAN_POINT('Ctrl Pts',(0.0700269035290348,-0.995644399133693,
1.17367754619314)) ;
#47250=CARTESIAN_POINT('Ctrl Pts',(0.255196528980468,-0.983684703017166,
1.15706829122464)) ;
#47251=CARTESIAN_POINT('Ctrl Pts',(0.40137680267713,-0.973210034697463,
1.11481385257197)) ;
#47252=CARTESIAN_POINT('Ctrl Pts',(0.67501512213282,-0.951439899620111,
0.974725872169565)) ;
#47253=CARTESIAN_POINT('Ctrl Pts',(0.798818187161842,-0.94034255841405,
0.876150002104573)) ;
#47254=CARTESIAN_POINT('Ctrl Pts',(0.996198613610554,-0.919896337867135,
0.641321507089482)) ;
#47255=CARTESIAN_POINT('Ctrl Pts',(1.06983935303753,-0.91109670451278,0.509067697275494)) ;
#47256=CARTESIAN_POINT('Ctrl Pts',(1.16420733489943,-0.890709556561418,
0.221550080315643)) ;
#47257=CARTESIAN_POINT('Ctrl Pts',(1.18310120566659,-0.879873775266811,
0.0687342954321408)) ;
#47258=CARTESIAN_POINT('Ctrl Pts',(1.16121537941864,-0.858061178187506,
-0.238886267625975)) ;
#47259=CARTESIAN_POINT('Ctrl Pts',(1.11932676411979,-0.847298992122945,
-0.390664147393342)) ;
#47260=CARTESIAN_POINT('Ctrl Pts',(0.98188157937219,-0.82800430468036,-0.66277491868477)) ;
#47261=CARTESIAN_POINT('Ctrl Pts',(0.890091424208338,-0.818609335264536,
-0.781744819650761)) ;
#47262=CARTESIAN_POINT('Ctrl Pts',(0.662862137417937,-0.797532518884636,
-0.982660013895455)) ;
#47263=CARTESIAN_POINT('Ctrl Pts',(0.52823683319041,-0.786483846628287,
-1.06111847054872)) ;
#47264=CARTESIAN_POINT('Ctrl Pts',(0.235245724512628,-0.764918500588585,
-1.16191020397607)) ;
#47265=CARTESIAN_POINT('Ctrl Pts',(0.079661845817216,-0.755159707229693,
-1.18279563163626)) ;
#47266=CARTESIAN_POINT('Ctrl Pts',(-0.225576153538807,-0.735719496716491,
-1.16315722188047)) ;
#47267=CARTESIAN_POINT('Ctrl Pts',(-0.372417354987327,-0.725341292371487,
-1.12476838448958)) ;
#47268=CARTESIAN_POINT('Ctrl Pts',(-0.648908395040247,-0.703663698131644,
-0.992231646806144)) ;
#47269=CARTESIAN_POINT('Ctrl Pts',(-0.774952444899368,-0.692556326854877,
-0.897254370444777)) ;
#47270=CARTESIAN_POINT('Ctrl Pts',(-0.978796169553678,-0.671901054676124,
-0.667724173774915)) ;
#47271=CARTESIAN_POINT('Ctrl Pts',(-1.05623767831092,-0.663070027598576,
-0.536897247170042)) ;
#47272=CARTESIAN_POINT('Ctrl Pts',(-1.15802196864285,-0.642844330631431,
-0.251656554984033)) ;
#47273=CARTESIAN_POINT('Ctrl Pts',(-1.18083758299913,-0.632075194358561,
-0.0997806572234279)) ;
#47274=CARTESIAN_POINT('Ctrl Pts',(-1.16715611539121,-0.61025481693953,
0.207949631076429)) ;
#47275=CARTESIAN_POINT('Ctrl Pts',(-1.12930643333218,-0.599415818249439,
0.36081079052065)) ;
#47276=CARTESIAN_POINT('Ctrl Pts',(-0.999113353668091,-0.579867007316284,
0.636505436348943)) ;
#47277=CARTESIAN_POINT('Ctrl Pts',(-0.91051501700737,-0.5707104587482,0.757855711459888)) ;
#47278=CARTESIAN_POINT('Ctrl Pts',(-0.689007310642716,-0.549783887762853,
0.964443186454003)) ;
#47279=CARTESIAN_POINT('Ctrl Pts',(-0.556912270785791,-0.538770378599761,
1.04629238738483)) ;
#47280=CARTESIAN_POINT('Ctrl Pts',(-0.280645631337244,-0.51813092533833,
1.14993623123353)) ;
#47281=CARTESIAN_POINT('Ctrl Pts',(-0.140822819567578,-0.508647601768867,
1.17524047358083)) ;
#47282=CARTESIAN_POINT('Ctrl Pts',(1.20840837336544E-13,-0.499999999999992,
1.17524047358083)) ;
#47283=CARTESIAN_POINT('Origin',(3.46944695195362E-16,1.71875,2.77555756156289E-16)) ;
#47284=CARTESIAN_POINT('',(-2.44853388629818E-15,-6.93889390390722E-17,
1.17524047358083)) ;
#47285=CARTESIAN_POINT('',(3.05062464863285E-15,-0.0624999999999969,1.17524047358083)) ;
#47286=CARTESIAN_POINT('',(5.49963941970804E-16,1.71875,1.17524047358083)) ;
#47287=CARTESIAN_POINT('Ctrl Pts',(5.48172618408671E-15,-0.0624999999999969,
1.17524047358083)) ;
#47288=CARTESIAN_POINT('Ctrl Pts',(-0.148863756462329,-0.0716413769988075,
1.17524047358083)) ;
#47289=CARTESIAN_POINT('Ctrl Pts',(-0.296501321439185,-0.0817101361724437,
1.14695911803628)) ;
#47290=CARTESIAN_POINT('Ctrl Pts',(-0.577730398749481,-0.102952751434487,
1.03489781920761)) ;
#47291=CARTESIAN_POINT('Ctrl Pts',(-0.70791218174543,-0.113935392844471,
0.950605408972408)) ;
#47292=CARTESIAN_POINT('Ctrl Pts',(-0.925193050987279,-0.134749025784293,
0.739882342016849)) ;
#47293=CARTESIAN_POINT('Ctrl Pts',(-1.0114453570678,-0.14376812017929,0.616745701812903)) ;
#47294=CARTESIAN_POINT('Ctrl Pts',(-1.13621629707524,-0.163502857584925,
0.338428956197801)) ;
#47295=CARTESIAN_POINT('Ctrl Pts',(-1.17104173892086,-0.174393915887241,
0.184833605993659)) ;
#47296=CARTESIAN_POINT('Ctrl Pts',(-1.17862495251038,-0.196209933636515,
-0.122835198382013)) ;
#47297=CARTESIAN_POINT('Ctrl Pts',(-1.15291451538109,-0.206924918680573,
-0.273947407553108)) ;
#47298=CARTESIAN_POINT('Ctrl Pts',(-1.04561263009304,-0.227028131315171,
-0.557460717199303)) ;
#47299=CARTESIAN_POINT('Ctrl Pts',(-0.965292388987877,-0.235921747370174,
-0.687227250187395)) ;
#47300=CARTESIAN_POINT('Ctrl Pts',(-0.756612097192965,-0.256730841667062,
-0.912718938330612)) ;
#47301=CARTESIAN_POINT('Ctrl Pts',(-0.628946947889343,-0.267840570816339,
-1.00495489370288)) ;
#47302=CARTESIAN_POINT('Ctrl Pts',(-0.350441736832899,-0.289438994590288,
-1.13176992081311)) ;
#47303=CARTESIAN_POINT('Ctrl Pts',(-0.203169603775975,-0.299740292845399,
-1.16724316717551)) ;
#47304=CARTESIAN_POINT('Ctrl Pts',(0.10316988606121,-0.319043810491533,
-1.18111821169802)) ;
#47305=CARTESIAN_POINT('Ctrl Pts',(0.259406451010041,-0.329079654765264,
-1.15690367490604)) ;
#47306=CARTESIAN_POINT('Ctrl Pts',(0.550860524019585,-0.350784890316052,
-1.04950402604207)) ;
#47307=CARTESIAN_POINT('Ctrl Pts',(0.683499565536527,-0.361806520981249,
-0.968367990394277)) ;
#47308=CARTESIAN_POINT('Ctrl Pts',(0.906224147383343,-0.38276530379844,
-0.762979645997387)) ;
#47309=CARTESIAN_POINT('Ctrl Pts',(0.995499624165027,-0.39196753531454,
-0.642139144322849)) ;
#47310=CARTESIAN_POINT('Ctrl Pts',(1.12724342088431,-0.411462527709364,
-0.367203495188301)) ;
#47311=CARTESIAN_POINT('Ctrl Pts',(1.16595749631123,-0.422285793008895,
-0.214564221952573)) ;
#47312=CARTESIAN_POINT('Ctrl Pts',(1.18138899932835,-0.444105823735235,
0.0931611769798911)) ;
#47313=CARTESIAN_POINT('Ctrl Pts',(1.15940729477125,-0.454889773301367,
0.245245984921959)) ;
#47314=CARTESIAN_POINT('Ctrl Pts',(1.05920543522115,-0.475150194460935,
0.530976388424197)) ;
#47315=CARTESIAN_POINT('Ctrl Pts',(0.98258090411365,-0.483969534936611,
0.662108179213888)) ;
#47316=CARTESIAN_POINT('Ctrl Pts',(0.780120151233503,-0.50458038576238,
0.892780814735941)) ;
#47317=CARTESIAN_POINT('Ctrl Pts',(0.654548434337712,-0.515686268917954,
0.988534222181722)) ;
#47318=CARTESIAN_POINT('Ctrl Pts',(0.378652346208475,-0.537384930557364,
1.12269566908047)) ;
#47319=CARTESIAN_POINT('Ctrl Pts',(0.231944420472717,-0.547784377265534,
1.16191450401602)) ;
#47320=CARTESIAN_POINT('Ctrl Pts',(0.0545377800954748,-0.559117348409257,
1.1742923822592)) ;
#47321=CARTESIAN_POINT('Ctrl Pts',(0.0272552647469167,-0.560826317592848,
1.17524047358083)) ;
#47322=CARTESIAN_POINT('Ctrl Pts',(4.16623745558835E-13,-0.562499999999971,
1.17524047358083)) ;
#47323=CARTESIAN_POINT('Ctrl Pts',(1.2066736498895E-13,-0.499999999999993,
1.17524047358083)) ;
#47324=CARTESIAN_POINT('Ctrl Pts',(0.0157279213843709,-0.499034184933935,
1.17524047358083)) ;
#47325=CARTESIAN_POINT('Ctrl Pts',(0.0314669663668242,-0.498056493301619,
1.17492475250529)) ;
#47326=CARTESIAN_POINT('Ctrl Pts',(0.197158826179065,-0.487645584755661,
1.16826376594166)) ;
#47327=CARTESIAN_POINT('Ctrl Pts',(0.344536563790507,-0.477365486927465,
1.13357140642765)) ;
#47328=CARTESIAN_POINT('Ctrl Pts',(0.623561267562816,-0.455789628905362,
1.00829265153272)) ;
#47329=CARTESIAN_POINT('Ctrl Pts',(0.751650560225984,-0.444680024415349,
0.916794850119542)) ;
#47330=CARTESIAN_POINT('Ctrl Pts',(0.961620797812825,-0.423830315427508,
0.692391844939811)) ;
#47331=CARTESIAN_POINT('Ctrl Pts',(1.04271468875434,-0.414914304009938,
0.562906866567344)) ;
#47332=CARTESIAN_POINT('Ctrl Pts',(1.15148401473377,-0.394844034949927,
0.279858156387584)) ;
#47333=CARTESIAN_POINT('Ctrl Pts',(1.17796078895353,-0.384144101172343,
0.128958213506981)) ;
#47334=CARTESIAN_POINT('Ctrl Pts',(1.1719980207065,-0.362330698347518,-0.178673712888099)) ;
#47335=CARTESIAN_POINT('Ctrl Pts',(1.13797935938651,-0.351426530807025,
-0.33245394117964)) ;
#47336=CARTESIAN_POINT('Ctrl Pts',(1.01465442966734,-0.331642805467273,
-0.611461558029465)) ;
#47337=CARTESIAN_POINT('Ctrl Pts',(0.929022334265141,-0.322654585934169,
-0.735075718348283)) ;
#47338=CARTESIAN_POINT('Ctrl Pts',(0.712861370794559,-0.301871144438001,
-0.946886946042434)) ;
#47339=CARTESIAN_POINT('Ctrl Pts',(0.58319249722894,-0.290897365638977,
-1.03181776469222)) ;
#47340=CARTESIAN_POINT('Ctrl Pts',(0.29630395858214,-0.269163983384795,
-1.14791905051678)) ;
#47341=CARTESIAN_POINT('Ctrl Pts',(0.141606825355615,-0.25875931516526,
-1.17703349823979)) ;
#47342=CARTESIAN_POINT('Ctrl Pts',(-0.163814445446772,-0.2398735308139,
-1.17335054150085)) ;
#47343=CARTESIAN_POINT('Ctrl Pts',(-0.311702081140799,-0.22971536530763,
-1.14298054656693)) ;
#47344=CARTESIAN_POINT('Ctrl Pts',(-0.593450382682682,-0.208274771929066,
-1.0262344449978)) ;
#47345=CARTESIAN_POINT('Ctrl Pts',(-0.723811054306731,-0.197171609466349,
-0.938852489697176)) ;
#47346=CARTESIAN_POINT('Ctrl Pts',(-0.940882920239149,-0.176101524754104,
-0.720533998331314)) ;
#47347=CARTESIAN_POINT('Ctrl Pts',(-1.02628296898357,-0.167019286382454,
-0.592593192331669)) ;
#47348=CARTESIAN_POINT('Ctrl Pts',(-1.14310264626327,-0.147132496588164,
-0.312132069261559)) ;
#47349=CARTESIAN_POINT('Ctrl Pts',(-1.17375434493936,-0.136519917593742,
-0.162464080901736)) ;
#47350=CARTESIAN_POINT('Ctrl Pts',(-1.17667790497532,-0.114633942569097,
0.146191322931168)) ;
#47351=CARTESIAN_POINT('Ctrl Pts',(-1.14656204074406,-0.103568168772267,
0.302250665781474)) ;
#47352=CARTESIAN_POINT('Ctrl Pts',(-1.0297060599707,-0.0834604539426645,
0.585827469369135)) ;
#47353=CARTESIAN_POINT('Ctrl Pts',(-0.947044314185684,-0.0745879331365558,
0.711759154062011)) ;
#47354=CARTESIAN_POINT('Ctrl Pts',(-0.73625789154082,-0.053950906669795,
0.928749610689681)) ;
#47355=CARTESIAN_POINT('Ctrl Pts',(-0.609083798106053,-0.0430235742996687,
1.01669145792555)) ;
#47356=CARTESIAN_POINT('Ctrl Pts',(-0.325737152011206,-0.0212557872096278,
1.13989789653917)) ;
#47357=CARTESIAN_POINT('Ctrl Pts',(-0.171855723771338,-0.0106321681509957,
1.17301481473308)) ;
#47358=CARTESIAN_POINT('Ctrl Pts',(-0.0106387770903632,-0.000654582620188146,
1.17520436830659)) ;
#47359=CARTESIAN_POINT('Ctrl Pts',(-0.00531867141127997,-0.000326607239120388,
1.17524047358083)) ;
#47360=CARTESIAN_POINT('Ctrl Pts',(-5.44703171456717E-15,3.46944695195361E-17,
1.17524047358083)) ;
#47361=CARTESIAN_POINT('Origin',(3.46944695195362E-16,1.71875,2.77555756156289E-16)) ;
#47362=CARTESIAN_POINT('',(-1.88715537221405E-13,0.499999999999977,1.17524047358083)) ;
#47363=CARTESIAN_POINT('',(-8.32241523838793E-14,0.437499999999993,1.17524047358083)) ;
#47364=CARTESIAN_POINT('',(5.49963941970804E-16,1.71875,1.17524047358083)) ;
#47365=CARTESIAN_POINT('Ctrl Pts',(-1.66998268709729E-13,0.437499999999993,
1.17524047358083)) ;
#47366=CARTESIAN_POINT('Ctrl Pts',(-0.017816889025783,0.436405906290418,
1.17524047358083)) ;
#47367=CARTESIAN_POINT('Ctrl Pts',(-0.0356475927526497,0.435296599925478,
1.17483531666615)) ;
#47368=CARTESIAN_POINT('Ctrl Pts',(-0.203474498162529,0.424719704494279,
1.16719054941927)) ;
#47369=CARTESIAN_POINT('Ctrl Pts',(-0.35074116224463,0.414417337248731,
1.13167767881478)) ;
#47370=CARTESIAN_POINT('Ctrl Pts',(-0.629219788395705,0.392817783737344,
1.00478474018186)) ;
#47371=CARTESIAN_POINT('Ctrl Pts',(-0.756863302708354,0.381708056764137,
0.912511373283748)) ;
#47372=CARTESIAN_POINT('Ctrl Pts',(-0.965478079711285,0.36090102991899,
0.686964524263308)) ;
#47373=CARTESIAN_POINT('Ctrl Pts',(-1.04575909549831,0.352008487250049,
0.557183679194484)) ;
#47374=CARTESIAN_POINT('Ctrl Pts',(-1.15298640618235,0.331903604566664,
0.273646817041186)) ;
#47375=CARTESIAN_POINT('Ctrl Pts',(-1.17865785708671,0.321187861874008,
0.12252392283852)) ;
#47376=CARTESIAN_POINT('Ctrl Pts',(-1.17099227410892,0.29937172754926,-0.185146525587731)) ;
#47377=CARTESIAN_POINT('Ctrl Pts',(-1.13612585809603,0.288481343739001,
-0.338732363507496)) ;
#47378=CARTESIAN_POINT('Ctrl Pts',(-1.01128147694235,0.268749101102935,
-0.617013925672573)) ;
#47379=CARTESIAN_POINT('Ctrl Pts',(-0.92499761161151,0.259728374148979,
-0.740126326392309)) ;
#47380=CARTESIAN_POINT('Ctrl Pts',(-0.707659781494743,0.238913208577674,
-0.950793963271697)) ;
#47381=CARTESIAN_POINT('Ctrl Pts',(-0.577451976646021,0.227930124001106,
-1.03505380219116)) ;
#47382=CARTESIAN_POINT('Ctrl Pts',(-0.289830594901794,0.206207888071383,
-1.14957137585777)) ;
#47383=CARTESIAN_POINT('Ctrl Pts',(-0.134961808647696,0.19587901894077,
-1.17781645643573)) ;
#47384=CARTESIAN_POINT('Ctrl Pts',(0.170536816874875,0.176927135094982,
-1.17240309477512)) ;
#47385=CARTESIAN_POINT('Ctrl Pts',(0.31833195220016,0.166743801259716,-1.14116299236951)) ;
#47386=CARTESIAN_POINT('Ctrl Pts',(0.599552627745338,0.145274570737449,
-1.02269528303885)) ;
#47387=CARTESIAN_POINT('Ctrl Pts',(0.729466435647479,0.134169329798734,
-0.934480712049055)) ;
#47388=CARTESIAN_POINT('Ctrl Pts',(0.945113748484863,0.113143004552156,
-0.714929091828199)) ;
#47389=CARTESIAN_POINT('Ctrl Pts',(1.02964344740617,0.104099930553232,-0.586679065011666)) ;
#47390=CARTESIAN_POINT('Ctrl Pts',(1.14485192050447,0.0841760461180767,
-0.305694800461991)) ;
#47391=CARTESIAN_POINT('Ctrl Pts',(1.17467217794547,0.0735453415167243,
-0.155771188739705)) ;
#47392=CARTESIAN_POINT('Ctrl Pts',(1.17581487774868,0.0516459156569779,
0.153073910682973)) ;
#47393=CARTESIAN_POINT('Ctrl Pts',(1.14476153163351,0.0405861484727693,
0.30904854296214)) ;
#47394=CARTESIAN_POINT('Ctrl Pts',(1.02619522438653,0.020527234767995,0.591937109865149)) ;
#47395=CARTESIAN_POINT('Ctrl Pts',(0.942830977195143,0.0116321861240577,
0.717316136360187)) ;
#47396=CARTESIAN_POINT('Ctrl Pts',(0.729193137971309,-0.00919364706669305,
0.934693233888779)) ;
#47397=CARTESIAN_POINT('Ctrl Pts',(0.599257568047615,-0.0202987964095113,
1.02286752841867)) ;
#47398=CARTESIAN_POINT('Ctrl Pts',(0.318011099999538,-0.0417666563563344,
1.14125190568622)) ;
#47399=CARTESIAN_POINT('Ctrl Pts',(0.170211367213076,-0.0519487785066309,
1.1724498685463)) ;
#47400=CARTESIAN_POINT('Ctrl Pts',(0.0136645921220641,-0.0616587775845467,
1.17518091428279)) ;
#47401=CARTESIAN_POINT('Ctrl Pts',(0.00683113258147283,-0.0620805160386885,
1.17524047358083)) ;
#47402=CARTESIAN_POINT('Ctrl Pts',(5.55128535529489E-15,-0.0624999999999967,
1.17524047358083)) ;
#47403=CARTESIAN_POINT('Ctrl Pts',(-5.58580959264532E-15,-1.30104260698261E-17,
1.17524047358083)) ;
#47404=CARTESIAN_POINT('Ctrl Pts',(0.150387712606244,0.00923495960059556,
1.17524047358083)) ;
#47405=CARTESIAN_POINT('Ctrl Pts',(0.299504882175791,0.0194152486344145,
1.14637608262904)) ;
#47406=CARTESIAN_POINT('Ctrl Pts',(0.581649964952125,0.0407716668309997,
1.03269145225507)) ;
#47407=CARTESIAN_POINT('Ctrl Pts',(0.711464153498591,0.0517479810585996,
0.947940812816467)) ;
#47408=CARTESIAN_POINT('Ctrl Pts',(0.927941859614262,0.0725399728462657,
0.736437031909328)) ;
#47409=CARTESIAN_POINT('Ctrl Pts',(1.01374931713132,0.0815366885848531,
0.612958112291061)) ;
#47410=CARTESIAN_POINT('Ctrl Pts',(1.13748362488098,0.10130657063834,0.33414572572495)) ;
#47411=CARTESIAN_POINT('Ctrl Pts',(1.17173069626048,0.112207059875292,0.180417372127794)) ;
#47412=CARTESIAN_POINT('Ctrl Pts',(1.17815196237782,0.134021264674389,-0.127225864418774)) ;
#47413=CARTESIAN_POINT('Ctrl Pts',(1.15189189723141,0.144725485355728,-0.278186265012975)) ;
#47414=CARTESIAN_POINT('Ctrl Pts',(1.04353784532397,0.164805092867427,-0.561366674309399)) ;
#47415=CARTESIAN_POINT('Ctrl Pts',(0.962663238417732,0.173714520435076,
-0.690931317950019)) ;
#47416=CARTESIAN_POINT('Ctrl Pts',(0.753058194864076,0.19455274892985,-0.915643041587181)) ;
#47417=CARTESIAN_POINT('Ctrl Pts',(0.625088625188735,0.2056624210965,-1.00735011816981)) ;
#47418=CARTESIAN_POINT('Ctrl Pts',(0.34621023025533,0.227244729882854,-1.13306423618887)) ;
#47419=CARTESIAN_POINT('Ctrl Pts',(0.198861988640031,0.237530859218139,
-1.16797780757678)) ;
#47420=CARTESIAN_POINT('Ctrl Pts',(-0.107685913283433,0.256807842291688,
-1.18074344368933)) ;
#47421=CARTESIAN_POINT('Ctrl Pts',(-0.264049422991349,0.266900965989962,
-1.15588270733456)) ;
#47422=CARTESIAN_POINT('Ctrl Pts',(-0.555198262685363,0.288632714640628,
-1.04720655642656)) ;
#47423=CARTESIAN_POINT('Ctrl Pts',(-0.687447928061904,0.299648562538409,
-0.965559208935909)) ;
#47424=CARTESIAN_POINT('Ctrl Pts',(-0.909300810834917,0.320584284569134,
-0.759311484724843)) ;
#47425=CARTESIAN_POINT('Ctrl Pts',(-0.998091138100098,0.329753514657127,
-0.638106010346577)) ;
#47426=CARTESIAN_POINT('Ctrl Pts',(-1.12872455349813,0.349287072452111,
-0.362626477782252)) ;
#47427=CARTESIAN_POINT('Ctrl Pts',(-1.16681971741147,0.36012164176838,-0.209827785290715)) ;
#47428=CARTESIAN_POINT('Ctrl Pts',(-1.18099786356303,0.38194199317296,0.0979021361303076)) ;
#47429=CARTESIAN_POINT('Ctrl Pts',(-1.15841877755348,0.392715366544137,
0.249837789203979)) ;
#47430=CARTESIAN_POINT('Ctrl Pts',(-1.05708362777342,0.412950937587882,
0.535217734363541)) ;
#47431=CARTESIAN_POINT('Ctrl Pts',(-0.979874387076045,0.421778365177155,
0.666131149349083)) ;
#47432=CARTESIAN_POINT('Ctrl Pts',(-0.776423383293504,0.442421042552534,
0.895986312377557)) ;
#47433=CARTESIAN_POINT('Ctrl Pts',(-0.650513068327186,0.453528027849362,
0.99118433750606)) ;
#47434=CARTESIAN_POINT('Ctrl Pts',(-0.374190124089755,0.475211675331599,
1.12418296205339)) ;
#47435=CARTESIAN_POINT('Ctrl Pts',(-0.227386317306555,0.485595945618796,
1.16280766348317)) ;
#47436=CARTESIAN_POINT('Ctrl Pts',(-0.0515081845879271,0.496807018632516,
1.17439476386601)) ;
#47437=CARTESIAN_POINT('Ctrl Pts',(-0.0257415650013721,0.498419270373064,
1.17524047358082)) ;
#47438=CARTESIAN_POINT('Ctrl Pts',(-3.77981038384781E-13,0.499999999999977,
1.17524047358083)) ;
#47439=CARTESIAN_POINT('Origin',(3.46944695195362E-16,1.71875,2.77555756156289E-16)) ;
#47440=CARTESIAN_POINT('',(-2.19540941881722E-13,0.999999999999973,1.17524047358083)) ;
#47441=CARTESIAN_POINT('',(-2.68861589338229E-13,0.93749999999997,1.17524047358083)) ;
#47442=CARTESIAN_POINT('',(5.49963941970804E-16,1.71875,1.17524047358083)) ;
#47443=CARTESIAN_POINT('',(0.94347795579564,1.17524047358083,-0.700742119235159)) ;
#47444=CARTESIAN_POINT('Ctrl Pts',(-4.39370761995406E-13,0.999999999999973,
1.17524047358083)) ;
#47445=CARTESIAN_POINT('Ctrl Pts',(0.106843190322386,1.00656099178002,1.17524047358087)) ;
#47446=CARTESIAN_POINT('Ctrl Pts',(0.213368336153847,1.01361875616957,1.16067774971801)) ;
#47447=CARTESIAN_POINT('Ctrl Pts',(0.466148916094986,1.03164907154231,1.08994760428343)) ;
#47448=CARTESIAN_POINT('Ctrl Pts',(0.605855680297113,1.04274604071748,1.01892824263296)) ;
#47449=CARTESIAN_POINT('Ctrl Pts',(0.845124236320189,1.06412841046368,0.830247305995036)) ;
#47450=CARTESIAN_POINT('Ctrl Pts',(0.943713350646115,1.07421852266424,0.716165369678224)) ;
#47451=CARTESIAN_POINT('Ctrl Pts',(1.09610658325736,1.09297021377989,0.451712413511906)) ;
#47452=CARTESIAN_POINT('Ctrl Pts',(1.14627242176894,1.1035481597673,0.302532850490821)) ;
#47453=CARTESIAN_POINT('Ctrl Pts',(1.185194327271,1.1252945917279,-0.0041545934619247)) ;
#47454=CARTESIAN_POINT('Ctrl Pts',(1.17454441508537,1.13624596978566,-0.15860062628145)) ;
#47455=CARTESIAN_POINT('Ctrl Pts',(1.09609503850357,1.15682667556352,-0.448847967141481)) ;
#47456=CARTESIAN_POINT('Ctrl Pts',(1.03129237683895,1.16565618612113,-0.582508937325451)) ;
#47457=CARTESIAN_POINT('Ctrl Pts',(0.943477955795638,1.17524047358083,-0.700742119235157)) ;
#47458=CARTESIAN_POINT('',(0.190653686692406,1.17524047358083,-1.15967294634871)) ;
#47459=CARTESIAN_POINT('Origin',(2.81025203108243E-15,1.17524047358083,
-1.11022302462516E-15)) ;
#47460=CARTESIAN_POINT('Ctrl Pts',(0.190653686690487,1.17524047358096,-1.15967294634902)) ;
#47461=CARTESIAN_POINT('Ctrl Pts',(0.334721572181544,1.16555387138265,-1.13598775684016)) ;
#47462=CARTESIAN_POINT('Ctrl Pts',(0.473089930863508,1.15527304834815,-1.08567024027228)) ;
#47463=CARTESIAN_POINT('Ctrl Pts',(0.724034634321941,1.13459622175091,-0.937113372977569)) ;
#47464=CARTESIAN_POINT('Ctrl Pts',(0.834519828985816,1.12437695843099,-0.840237138889637)) ;
#47465=CARTESIAN_POINT('Ctrl Pts',(1.01675905936992,1.10495423704233,-0.608051906254154)) ;
#47466=CARTESIAN_POINT('Ctrl Pts',(1.08575086392768,1.09611011380817,-0.473999592828079)) ;
#47467=CARTESIAN_POINT('Ctrl Pts',(1.17083816769886,1.07552627544959,-0.183708073540434)) ;
#47468=CARTESIAN_POINT('Ctrl Pts',(1.18478330659978,1.06461718036353,-0.0298583526371077)) ;
#47469=CARTESIAN_POINT('Ctrl Pts',(1.15263710342259,1.04283633695152,0.277314392081248)) ;
#47470=CARTESIAN_POINT('Ctrl Pts',(1.10574557383279,1.03218111653273,0.427583747574201)) ;
#47471=CARTESIAN_POINT('Ctrl Pts',(0.959283994206446,1.01321090337417,0.695118495130982)) ;
#47472=CARTESIAN_POINT('Ctrl Pts',(0.863430595265501,1.00343003623297,0.811138605254806)) ;
#47473=CARTESIAN_POINT('Ctrl Pts',(0.628978803774639,0.982168112369197,
1.00476515376881)) ;
#47474=CARTESIAN_POINT('Ctrl Pts',(0.491263975439452,0.971086219817788,
1.0788094017436)) ;
#47475=CARTESIAN_POINT('Ctrl Pts',(0.231716823142686,0.952338744278339,
1.15804755576006)) ;
#47476=CARTESIAN_POINT('Ctrl Pts',(0.116090981062413,0.94462887709724,1.17524047358088)) ;
#47477=CARTESIAN_POINT('Ctrl Pts',(-5.38250000126084E-13,0.93749999999997,
1.17524047358083)) ;
#47478=CARTESIAN_POINT('Origin',(0.,1.5,0.)) ;
#47479=CARTESIAN_POINT('',(2.44539079942923E-14,-1.24999999999999,1.5)) ;
#47480=CARTESIAN_POINT('',(5.94426045891414E-14,-1.3125,1.5)) ;
#47481=CARTESIAN_POINT('',(-1.83697019872103E-16,1.5,1.5)) ;
#47482=CARTESIAN_POINT('',(-1.05094390383305,-1.5,-1.07028823734364)) ;
#47483=CARTESIAN_POINT('Ctrl Pts',(1.19002030452009E-13,-1.3125,1.5)) ;
#47484=CARTESIAN_POINT('Ctrl Pts',(-0.125690544708079,-1.31854728915183,
1.5)) ;
#47485=CARTESIAN_POINT('Ctrl Pts',(-0.251130003993841,-1.32502121415508,
1.4842062166389)) ;
#47486=CARTESIAN_POINT('Ctrl Pts',(-0.565489283533066,-1.34239014330235,
1.40341101133005)) ;
#47487=CARTESIAN_POINT('Ctrl Pts',(-0.745894934843807,-1.35348619283281,
1.31642498227603)) ;
#47488=CARTESIAN_POINT('Ctrl Pts',(-1.05645955766431,-1.3749450764572,1.08181887755639)) ;
#47489=CARTESIAN_POINT('Ctrl Pts',(-1.18544422357363,-1.38512598373554,
0.938714210288529)) ;
#47490=CARTESIAN_POINT('Ctrl Pts',(-1.38685389066128,-1.40408354370044,
0.605093828083167)) ;
#47491=CARTESIAN_POINT('Ctrl Pts',(-1.45477162975192,-1.41437991998462,
0.416161440276449)) ;
#47492=CARTESIAN_POINT('Ctrl Pts',(-1.51252462564358,-1.43607724588768,
0.0256095740214394)) ;
#47493=CARTESIAN_POINT('Ctrl Pts',(-1.50293685043723,-1.44705355116319,
-0.171963920937831)) ;
#47494=CARTESIAN_POINT('Ctrl Pts',(-1.42232581449327,-1.46505639030648,
-0.496015025517027)) ;
#47495=CARTESIAN_POINT('Ctrl Pts',(-1.37068981709763,-1.47220607842093,
-0.62470941157705)) ;
#47496=CARTESIAN_POINT('Ctrl Pts',(-1.23381696495112,-1.48550538860935,
-0.864096994968711)) ;
#47497=CARTESIAN_POINT('Ctrl Pts',(-1.1492933800039,-1.49258560548561,-0.973716324451006)) ;
#47498=CARTESIAN_POINT('Ctrl Pts',(-1.05094390383214,-1.50000000000007,
-1.07028823734453)) ;
#47499=CARTESIAN_POINT('',(0.,-1.5,-1.5)) ;
#47500=CARTESIAN_POINT('Origin',(0.,-1.5,0.)) ;
#47501=CARTESIAN_POINT('Ctrl Pts',(2.18575157973078E-15,-1.5,-1.5)) ;
#47502=CARTESIAN_POINT('Ctrl Pts',(-0.138596334074203,-1.49333178076779,
-1.5)) ;
#47503=CARTESIAN_POINT('Ctrl Pts',(-0.276578903789693,-1.48615954753798,
-1.48079242503239)) ;
#47504=CARTESIAN_POINT('Ctrl Pts',(-0.548119381515871,-1.47095166696557,
-1.40363062815888)) ;
#47505=CARTESIAN_POINT('Ctrl Pts',(-0.67987312768868,-1.46297740045344,
-1.34476121618135)) ;
#47506=CARTESIAN_POINT('Ctrl Pts',(-0.9693345679576,-1.44397019985451,-1.16186391599752)) ;
#47507=CARTESIAN_POINT('Ctrl Pts',(-1.11466773993113,-1.43312791769337,
-1.0232661960797)) ;
#47508=CARTESIAN_POINT('Ctrl Pts',(-1.33768338804696,-1.41355051431735,
-0.704754107962303)) ;
#47509=CARTESIAN_POINT('Ctrl Pts',(-1.41608739796283,-1.40443849522844,
-0.52989291411165)) ;
#47510=CARTESIAN_POINT('Ctrl Pts',(-1.5049026353994,-1.38356148693885,-0.154106764899098)) ;
#47511=CARTESIAN_POINT('Ctrl Pts',(-1.51213717096723,-1.37256640287649,
0.0438047482233367)) ;
#47512=CARTESIAN_POINT('Ctrl Pts',(-1.44932925607157,-1.3508053928519,0.435502928665868)) ;
#47513=CARTESIAN_POINT('Ctrl Pts',(-1.37819971812457,-1.34061157337981,
0.625095293096029)) ;
#47514=CARTESIAN_POINT('Ctrl Pts',(-1.17058637322926,-1.32139662500094,
0.957236573047296)) ;
#47515=CARTESIAN_POINT('Ctrl Pts',(-1.03915094756602,-1.31114876375226,
1.09850674283675)) ;
#47516=CARTESIAN_POINT('Ctrl Pts',(-0.724349226230084,-1.28961552393313,
1.32845080066116)) ;
#47517=CARTESIAN_POINT('Ctrl Pts',(-0.542233928925934,-1.27851587207399,
1.41260531982395)) ;
#47518=CARTESIAN_POINT('Ctrl Pts',(-0.234427210984566,-1.26166095877703,
1.48624532412904)) ;
#47519=CARTESIAN_POINT('Ctrl Pts',(-0.117295539887556,-1.25564338429406,
1.5)) ;
#47520=CARTESIAN_POINT('Ctrl Pts',(4.81906181626357E-14,-1.24999999999999,
1.5)) ;
#47521=CARTESIAN_POINT('Origin',(0.,1.5,0.)) ;
#47522=CARTESIAN_POINT('',(1.25863447800723E-13,-0.749999999999985,1.5)) ;
#47523=CARTESIAN_POINT('',(1.1883828150139E-13,-0.81249999999999,1.5)) ;
#47524=CARTESIAN_POINT('',(-1.83697019872103E-16,1.5,1.5)) ;
#47525=CARTESIAN_POINT('Ctrl Pts',(2.37860260022652E-13,-0.81249999999999,
1.5)) ;
#47526=CARTESIAN_POINT('Ctrl Pts',(-0.156447465110858,-0.820027082174664,
1.5)) ;
#47527=CARTESIAN_POINT('Ctrl Pts',(-0.312164809475088,-0.828198750725344,
1.47553028423322)) ;
#47528=CARTESIAN_POINT('Ctrl Pts',(-0.649100769465223,-0.847436020155903,
1.36657878633297)) ;
#47529=CARTESIAN_POINT('Ctrl Pts',(-0.822902367070701,-0.858493925193746,
1.26952740245995)) ;
#47530=CARTESIAN_POINT('Ctrl Pts',(-1.11762648369567,-0.879650906765802,
1.01835321007618)) ;
#47531=CARTESIAN_POINT('Ctrl Pts',(-1.23751114978123,-0.889238109349478,
0.868714031709184)) ;
#47532=CARTESIAN_POINT('Ctrl Pts',(-1.41915748444322,-0.90833829037694,
0.524910773214875)) ;
#47533=CARTESIAN_POINT('Ctrl Pts',(-1.47615258074904,-0.919033448908922,
0.332397919639227)) ;
#47534=CARTESIAN_POINT('Ctrl Pts',(-1.51142533493793,-0.940813655782774,
-0.0596458040901028)) ;
#47535=CARTESIAN_POINT('Ctrl Pts',(-1.49090868354231,-0.951681828986031,
-0.255272921748749)) ;
#47536=CARTESIAN_POINT('Ctrl Pts',(-1.37736667279861,-0.972163237090842,
-0.623938267635399)) ;
#47537=CARTESIAN_POINT('Ctrl Pts',(-1.28689333739595,-0.980971534163011,
-0.793939874160591)) ;
#47538=CARTESIAN_POINT('Ctrl Pts',(-1.04114745712756,-1.00124754387222,
-1.0982318733166)) ;
#47539=CARTESIAN_POINT('Ctrl Pts',(-0.885409852125076,-1.01232423013715,
-1.22724713434068)) ;
#47540=CARTESIAN_POINT('Ctrl Pts',(-0.539253545854058,-1.03413578891522,
-1.41290294052909)) ;
#47541=CARTESIAN_POINT('Ctrl Pts',(-0.353564236997969,-1.04466712776859,
-1.47040782188932)) ;
#47542=CARTESIAN_POINT('Ctrl Pts',(0.0323067062935163,-1.06439721558525,
-1.51234290434375)) ;
#47543=CARTESIAN_POINT('Ctrl Pts',(0.228921251204819,-1.07364538754622,
-1.49526928635465)) ;
#47544=CARTESIAN_POINT('Ctrl Pts',(0.606732761779437,-1.09485823271693,
-1.38599559220871)) ;
#47545=CARTESIAN_POINT('Ctrl Pts',(0.78397190838898,-1.10594048180573,-1.29402183202991)) ;
#47546=CARTESIAN_POINT('Ctrl Pts',(1.08686896974953,-1.12725901834733,-1.051187616272)) ;
#47547=CARTESIAN_POINT('Ctrl Pts',(1.21137930856031,-1.13722951519011,-0.904868726577733)) ;
#47548=CARTESIAN_POINT('Ctrl Pts',(1.4031642124512,-1.15604084125592,-0.566264857393262)) ;
#47549=CARTESIAN_POINT('Ctrl Pts',(1.46576524891775,-1.16663659132274,-0.37554135619049)) ;
#47550=CARTESIAN_POINT('Ctrl Pts',(1.51259069068335,-1.18837829937752,0.0158093887954927)) ;
#47551=CARTESIAN_POINT('Ctrl Pts',(1.49767343362296,-1.1993062118098,0.212511812576511)) ;
#47552=CARTESIAN_POINT('Ctrl Pts',(1.39459172544617,-1.21995828168816,0.584249070387106)) ;
#47553=CARTESIAN_POINT('Ctrl Pts',(1.30929591411423,-1.22884778908545,0.756287452464687)) ;
#47554=CARTESIAN_POINT('Ctrl Pts',(1.07255114321248,-1.24888841128061,1.06769587986244)) ;
#47555=CARTESIAN_POINT('Ctrl Pts',(0.920126566016231,-1.25993973528819,
1.20153643210929)) ;
#47556=CARTESIAN_POINT('Ctrl Pts',(0.578370341808044,-1.28182365534903,
1.39741841016814)) ;
#47557=CARTESIAN_POINT('Ctrl Pts',(0.393835703366298,-1.2924461640788,1.46020535490243)) ;
#47558=CARTESIAN_POINT('Ctrl Pts',(0.13521340142217,-1.30586770692904,1.49543393057343)) ;
#47559=CARTESIAN_POINT('Ctrl Pts',(0.0675765704749157,-1.30924872073712,
1.5)) ;
#47560=CARTESIAN_POINT('Ctrl Pts',(1.19068906198155E-13,-1.3125,1.5)) ;
#47561=CARTESIAN_POINT('Ctrl Pts',(4.90915130084568E-14,-1.24999999999999,
1.5)) ;
#47562=CARTESIAN_POINT('Ctrl Pts',(0.07522788002324,-1.24638059693483,1.5)) ;
#47563=CARTESIAN_POINT('Ctrl Pts',(0.150507881150062,-1.24260150705645,
1.49434155112345)) ;
#47564=CARTESIAN_POINT('Ctrl Pts',(0.416459553793433,-1.22868401181681,
1.45395353187258)) ;
#47565=CARTESIAN_POINT('Ctrl Pts',(0.600276122090132,-1.21801338726496,
1.38819068356874)) ;
#47566=CARTESIAN_POINT('Ctrl Pts',(0.937459127338934,-1.1962224867055,1.18773635996788)) ;
#47567=CARTESIAN_POINT('Ctrl Pts',(1.08651459968785,-1.18531157658795,1.05311524699077)) ;
#47568=CARTESIAN_POINT('Ctrl Pts',(1.31823172790811,-1.16548099578163,0.740560177024522)) ;
#47569=CARTESIAN_POINT('Ctrl Pts',(1.40140246253754,-1.15653696644918,0.567665396084969)) ;
#47570=CARTESIAN_POINT('Ctrl Pts',(1.50012619162202,-1.13581521641982,0.194673895556624)) ;
#47571=CARTESIAN_POINT('Ctrl Pts',(1.51270127932233,-1.12486502884897,-0.0024294807186321)) ;
#47572=CARTESIAN_POINT('Ctrl Pts',(1.46105722910734,-1.10313814923197,-0.393513313824723)) ;
#47573=CARTESIAN_POINT('Ctrl Pts',(1.3960922028536,-1.09262939091854,-0.583444554325999)) ;
#47574=CARTESIAN_POINT('Ctrl Pts',(1.20008336997013,-1.07385392283904,-0.919864147901511)) ;
#47575=CARTESIAN_POINT('Ctrl Pts',(1.07358713734848,-1.06374269118958,-1.0647705854153)) ;
#47576=CARTESIAN_POINT('Ctrl Pts',(0.767348684105939,-1.0423638998445,-1.30398651359086)) ;
#47577=CARTESIAN_POINT('Ctrl Pts',(0.588703928541707,-1.03127443753244,
-1.39378536368201)) ;
#47578=CARTESIAN_POINT('Ctrl Pts',(0.209873430922041,-1.01015376126538,
-1.49797603996222)) ;
#47579=CARTESIAN_POINT('Ctrl Pts',(0.0137333074789716,-1.00100912536654,
-1.51254172688592)) ;
#47580=CARTESIAN_POINT('Ctrl Pts',(-0.371192239473193,-0.981198968126641,
-1.46608667070176)) ;
#47581=CARTESIAN_POINT('Ctrl Pts',(-0.556395397747934,-0.970626859815039,
-1.40627205133812)) ;
#47582=CARTESIAN_POINT('Ctrl Pts',(-0.900665850508364,-0.948781621036587,
-1.21613737103961)) ;
#47583=CARTESIAN_POINT('Ctrl Pts',(-1.05497403477983,-0.937714890204883,
-1.08500467628011)) ;
#47584=CARTESIAN_POINT('Ctrl Pts',(-1.29679747167913,-0.917540931357973,
-0.777592636961856)) ;
#47585=CARTESIAN_POINT('Ctrl Pts',(-1.38500644009541,-0.908706039897536,
-0.606708718155526)) ;
#47586=CARTESIAN_POINT('Ctrl Pts',(-1.49400139301044,-0.888149858014107,
-0.236697444253813)) ;
#47587=CARTESIAN_POINT('Ctrl Pts',(-1.5120883063272,-0.877254631314325,
-0.0405833636577428)) ;
#47588=CARTESIAN_POINT('Ctrl Pts',(-1.47179007933231,-0.855488831503584,
0.351201032935604)) ;
#47589=CARTESIAN_POINT('Ctrl Pts',(-1.41234983298357,-0.844835759900771,
0.54295632178624)) ;
#47590=CARTESIAN_POINT('Ctrl Pts',(-1.22628881776183,-0.825860517668724,
0.884510681963101)) ;
#47591=CARTESIAN_POINT('Ctrl Pts',(-1.10440403198004,-0.816116121019566,
1.0327035387692)) ;
#47592=CARTESIAN_POINT('Ctrl Pts',(-0.806135051990802,-0.794888528982598,
1.28027982443691)) ;
#47593=CARTESIAN_POINT('Ctrl Pts',(-0.630827416060365,-0.783818836307302,
1.37514702836123)) ;
#47594=CARTESIAN_POINT('Ctrl Pts',(-0.298684002099519,-0.764992300162682,
1.47761306118797)) ;
#47595=CARTESIAN_POINT('Ctrl Pts',(-0.149642595802423,-0.757199682747379,
1.5)) ;
#47596=CARTESIAN_POINT('Ctrl Pts',(2.5358187771829E-13,-0.749999999999985,
1.5)) ;
#47597=CARTESIAN_POINT('Origin',(0.,1.5,0.)) ;
#47598=CARTESIAN_POINT('',(2.44539079942923E-14,-0.249999999999995,1.5)) ;
#47599=CARTESIAN_POINT('',(6.9856727510751E-15,-0.3125,1.5)) ;
#47600=CARTESIAN_POINT('',(-1.83697019872103E-16,1.5,1.5)) ;
#47601=CARTESIAN_POINT('Ctrl Pts',(1.46410661372443E-14,-0.3125,1.5)) ;
#47602=CARTESIAN_POINT('Ctrl Pts',(-0.187010746043016,-0.32149755871411,
1.5)) ;
#47603=CARTESIAN_POINT('Ctrl Pts',(-0.372522155022534,-0.331394385307366,
1.46502942837889)) ;
#47604=CARTESIAN_POINT('Ctrl Pts',(-0.729433956821984,-0.352448532324359,
1.32526951030474)) ;
#47605=CARTESIAN_POINT('Ctrl Pts',(-0.896175160711237,-0.363430481795517,
1.21872356619442)) ;
#47606=CARTESIAN_POINT('Ctrl Pts',(-1.17491701108803,-0.384259579430114,
0.951671098397219)) ;
#47607=CARTESIAN_POINT('Ctrl Pts',(-1.28587778498005,-0.393312773348132,
0.795370079733538)) ;
#47608=CARTESIAN_POINT('Ctrl Pts',(-1.44726955852417,-0.412969136442091,
0.441555544042314)) ;
#47609=CARTESIAN_POINT('Ctrl Pts',(-1.49299246551635,-0.423833555841407,
0.245995994854643)) ;
#47610=CARTESIAN_POINT('Ctrl Pts',(-1.50535850109774,-0.44563386772807,
-0.146409619105293)) ;
#47611=CARTESIAN_POINT('Ctrl Pts',(-1.47388303399498,-0.456357986138421,
-0.339443750491626)) ;
#47612=CARTESIAN_POINT('Ctrl Pts',(-1.33962971691653,-0.476487789999139,
-0.701780219984592)) ;
#47613=CARTESIAN_POINT('Ctrl Pts',(-1.23855816416065,-0.485348762111955,
-0.867801104486143)) ;
#47614=CARTESIAN_POINT('Ctrl Pts',(-0.974770975084767,-0.506083106736852,
-1.15734469711718)) ;
#47615=CARTESIAN_POINT('Ctrl Pts',(-0.812759703657768,-0.517183229195444,
-1.27633735211607)) ;
#47616=CARTESIAN_POINT('Ctrl Pts',(-0.45858526139189,-0.538796477123096,
-1.44096614876463)) ;
#47617=CARTESIAN_POINT('Ctrl Pts',(-0.271009539442144,-0.549119454060885,
-1.48770263784166)) ;
#47618=CARTESIAN_POINT('Ctrl Pts',(0.119102093778023,-0.56846525435471,
-1.50845827905837)) ;
#47619=CARTESIAN_POINT('Ctrl Pts',(0.318052049351352,-0.578375637986886,
-1.4793593413999)) ;
#47620=CARTESIAN_POINT('Ctrl Pts',(0.690607371195689,-0.600004849340496,
-1.34599247873446)) ;
#47621=CARTESIAN_POINT('Ctrl Pts',(0.860852321760142,-0.611028519610325,
-1.24401325313029)) ;
#47622=CARTESIAN_POINT('Ctrl Pts',(1.14740420182817,-0.632019727786263,
-0.984652174078658)) ;
#47623=CARTESIAN_POINT('Ctrl Pts',(1.26270901412663,-0.64129791484719,-0.831637532750416)) ;
#47624=CARTESIAN_POINT('Ctrl Pts',(1.43407232346488,-0.660684006756509,
-0.4826878783827)) ;
#47625=CARTESIAN_POINT('Ctrl Pts',(1.48535296306111,-0.671469994454859,
-0.288540099812428)) ;
#47626=CARTESIAN_POINT('Ctrl Pts',(1.50896036510848,-0.693269776161453,
0.103855970906278)) ;
#47627=CARTESIAN_POINT('Ctrl Pts',(1.48283917680271,-0.704068836163023,
0.29823905093455)) ;
#47628=CARTESIAN_POINT('Ctrl Pts',(1.35875189168508,-0.724373392606975,
0.663721066925711)) ;
#47629=CARTESIAN_POINT('Ctrl Pts',(1.26294128670969,-0.733172592590258,
0.831691808807288)) ;
#47630=CARTESIAN_POINT('Ctrl Pts',(1.0080442938249,-0.753683385620307,1.12858581551606)) ;
#47631=CARTESIAN_POINT('Ctrl Pts',(0.84906092268456,-0.764776600734295,
1.25257428324593)) ;
#47632=CARTESIAN_POINT('Ctrl Pts',(0.498700007418968,-0.786496539143091,
1.42764915973622)) ;
#47633=CARTESIAN_POINT('Ctrl Pts',(0.311980955151472,-0.796926476589065,
1.47972002252289)) ;
#47634=CARTESIAN_POINT('Ctrl Pts',(0.0803526425168444,-0.808589245183692,
1.49838768597481)) ;
#47635=CARTESIAN_POINT('Ctrl Pts',(0.0401544197174351,-0.81056806958058,
1.5)) ;
#47636=CARTESIAN_POINT('Ctrl Pts',(2.37860260022652E-13,-0.81249999999999,
1.5)) ;
#47637=CARTESIAN_POINT('Ctrl Pts',(2.51910592621317E-13,-0.749999999999984,
1.5)) ;
#47638=CARTESIAN_POINT('Ctrl Pts',(0.0461416120551636,-0.747780010654926,
1.5)) ;
#47639=CARTESIAN_POINT('Ctrl Pts',(0.0923346900483627,-0.745498408059054,
1.49787106459072)) ;
#47640=CARTESIAN_POINT('Ctrl Pts',(0.329943863327776,-0.733454686588535,
1.47584825211639)) ;
#47641=CARTESIAN_POINT('Ctrl Pts',(0.516238107926601,-0.722980052420667,
1.42143251887597)) ;
#47642=CARTESIAN_POINT('Ctrl Pts',(0.864824462259465,-0.701218455313852,
1.2417842995603)) ;
#47643=CARTESIAN_POINT('Ctrl Pts',(1.02242731062005,-0.690131191238374,
1.11561893362118)) ;
#47644=CARTESIAN_POINT('Ctrl Pts',(1.27338820842905,-0.669720803380355,
0.81552199645074)) ;
#47645=CARTESIAN_POINT('Ctrl Pts',(1.36689330998072,-0.660926783329383,
0.646682099928811)) ;
#47646=CARTESIAN_POINT('Ctrl Pts',(1.48645525637395,-0.64054574751106,0.279823455199)) ;
#47647=CARTESIAN_POINT('Ctrl Pts',(1.51017696617209,-0.629715942961133,
0.0848869733003025)) ;
#47648=CARTESIAN_POINT('Ctrl Pts',(1.48156266081736,-0.607922189659522,
-0.307400586128696)) ;
#47649=CARTESIAN_POINT('Ctrl Pts',(1.42782270120019,-0.597174010873431,
-0.500867804278345)) ;
#47650=CARTESIAN_POINT('Ctrl Pts',(1.25203889624671,-0.577909943419593,
-0.847621018447427)) ;
#47651=CARTESIAN_POINT('Ctrl Pts',(1.13477837984287,-0.568508627404166,
-0.999183222668732)) ;
#47652=CARTESIAN_POINT('Ctrl Pts',(0.844728033590153,-0.547445955347855,
-1.25505748023326)) ;
#47653=CARTESIAN_POINT('Ctrl Pts',(0.672946332215184,-0.536406433221943,
-1.35494564217399)) ;
#47654=CARTESIAN_POINT('Ctrl Pts',(0.299208731678686,-0.514863106619634,
-1.483172887029)) ;
#47655=CARTESIAN_POINT('Ctrl Pts',(0.100766701449236,-0.505117175315716,
-1.50968526474447)) ;
#47656=CARTESIAN_POINT('Ctrl Pts',(-0.288472818487683,-0.485688724200375,
-1.48444364943667)) ;
#47657=CARTESIAN_POINT('Ctrl Pts',(-0.475702357207199,-0.475319311309763,
-1.43543585911451)) ;
#47658=CARTESIAN_POINT('Ctrl Pts',(-0.828290876262396,-0.453658618108879,
-1.26635213305172)) ;
#47659=CARTESIAN_POINT('Ctrl Pts',(-0.989031976371569,-0.44256031447766,
-1.1452249545814)) ;
#47660=CARTESIAN_POINT('Ctrl Pts',(-1.24904449455747,-0.421920316029762,
-0.85253990255895)) ;
#47661=CARTESIAN_POINT('Ctrl Pts',(-1.34787241514442,-0.413094081662667,
-0.685693469927933)) ;
#47662=CARTESIAN_POINT('Ctrl Pts',(-1.4778181443911,-0.392889717508791,
-0.322014915158169)) ;
#47663=CARTESIAN_POINT('Ctrl Pts',(-1.50703130418987,-0.382132857700582,
-0.1283914386104)) ;
#47664=CARTESIAN_POINT('Ctrl Pts',(-1.48990386914471,-0.360330572743572,
0.264049690615775)) ;
#47665=CARTESIAN_POINT('Ctrl Pts',(-1.44182082693689,-0.349498281946545,
0.459030924962268)) ;
#47666=CARTESIAN_POINT('Ctrl Pts',(-1.27619684671042,-0.32995577793014,
0.810795997257542)) ;
#47667=CARTESIAN_POINT('Ctrl Pts',(-1.16340334266401,-0.320815927649413,
0.965700303810776)) ;
#47668=CARTESIAN_POINT('Ctrl Pts',(-0.881360542847993,-0.299917888861523,
1.22951724098448)) ;
#47669=CARTESIAN_POINT('Ctrl Pts',(-0.713126432759514,-0.288917248829942,
1.33415025588196)) ;
#47670=CARTESIAN_POINT('Ctrl Pts',(-0.360105689805461,-0.26823254479493,
1.46734973822026)) ;
#47671=CARTESIAN_POINT('Ctrl Pts',(-0.180705529985591,-0.258694198865097,
1.5)) ;
#47672=CARTESIAN_POINT('Ctrl Pts',(4.90926743701436E-14,-0.249999999999995,
1.5)) ;
#47673=CARTESIAN_POINT('Origin',(0.,1.5,0.)) ;
#47674=CARTESIAN_POINT('',(-3.49720252756921E-15,0.250000000000002,1.5)) ;
#47675=CARTESIAN_POINT('',(-4.54712573957423E-14,0.187499999999993,1.5)) ;
#47676=CARTESIAN_POINT('',(-1.83697019872103E-16,1.5,1.5)) ;
#47677=CARTESIAN_POINT('Ctrl Pts',(-9.07588177716125E-14,0.187499999999994,
1.5)) ;
#47678=CARTESIAN_POINT('Ctrl Pts',(-0.0237189864434504,0.186358819732662,
1.5)) ;
#47679=CARTESIAN_POINT('Ctrl Pts',(-0.0474577649910852,0.185201059899418,
1.49943741655724)) ;
#47680=CARTESIAN_POINT('Ctrl Pts',(-0.262459822908907,0.17457297797897,
1.48922095546663)) ;
#47681=CARTESIAN_POINT('Ctrl Pts',(-0.450194841475407,0.164273189929587,
1.44359517620589)) ;
#47682=CARTESIAN_POINT('Ctrl Pts',(-0.805124481113827,0.142684229431146,
1.28114876722784)) ;
#47683=CARTESIAN_POINT('Ctrl Pts',(-0.967746636206636,0.131583821193572,
1.16320390573225)) ;
#47684=CARTESIAN_POINT('Ctrl Pts',(-1.23337408545708,0.110803802267297,
0.875203462372997)) ;
#47685=CARTESIAN_POINT('Ctrl Pts',(-1.33554531695723,0.101921319526277,
0.709583751472954)) ;
#47686=CARTESIAN_POINT('Ctrl Pts',(-1.47189435169531,0.0818280748851064,
0.347905347931908)) ;
#47687=CARTESIAN_POINT('Ctrl Pts',(-1.50446685481494,0.0711204066738244,
0.155167320128844)) ;
#47688=CARTESIAN_POINT('Ctrl Pts',(-1.49441590282142,0.0493222220689783,
-0.23720000275839)) ;
#47689=CARTESIAN_POINT('Ctrl Pts',(-1.44984377558211,0.0384427620859756,
-0.43303028245246)) ;
#47690=CARTESIAN_POINT('Ctrl Pts',(-1.29051485664985,0.018731362500822,
-0.787835474985263)) ;
#47691=CARTESIAN_POINT('Ctrl Pts',(-1.18044177811369,0.00971574318362152,
-0.944818380459478)) ;
#47692=CARTESIAN_POINT('Ctrl Pts',(-0.901901541919688,-0.0111847314112764,
-1.21478962483548)) ;
#47693=CARTESIAN_POINT('Ctrl Pts',(-0.733997449933338,-0.0222694381140607,
-1.32302064801658)) ;
#47694=CARTESIAN_POINT('Ctrl Pts',(-0.372671975906577,-0.0436089300705782,
-1.46540827936792)) ;
#47695=CARTESIAN_POINT('Ctrl Pts',(-0.183770006155042,-0.0536354113071329,
-1.50082620537561)) ;
#47696=CARTESIAN_POINT('Ctrl Pts',(0.205428255104891,-0.0724084659494439,
-1.49910740097208)) ;
#47697=CARTESIAN_POINT('Ctrl Pts',(0.402051497713194,-0.0829904980857595,
-1.45871569021124)) ;
#47698=CARTESIAN_POINT('Ctrl Pts',(0.765039896519852,-0.104725751684374,
-1.3049609099523)) ;
#47699=CARTESIAN_POINT('Ctrl Pts',(0.928411042654205,-0.115660845279063,
-1.19426466613892)) ;
#47700=CARTESIAN_POINT('Ctrl Pts',(1.19983378457874,-0.136334949627821,
-0.920114888926562)) ;
#47701=CARTESIAN_POINT('Ctrl Pts',(1.30674418549408,-0.145240331171075,
-0.760674038920638)) ;
#47702=CARTESIAN_POINT('Ctrl Pts',(1.45944177193774,-0.165249915641916,
-0.400501518445528)) ;
#47703=CARTESIAN_POINT('Ctrl Pts',(1.49989710280014,-0.176297274481281,
-0.20164905933698)) ;
#47704=CARTESIAN_POINT('Ctrl Pts',(1.50009856498918,-0.19818935744411,0.192408433993937)) ;
#47705=CARTESIAN_POINT('Ctrl Pts',(1.46287970752877,-0.208823144729875,
0.383816605137735)) ;
#47706=CARTESIAN_POINT('Ctrl Pts',(1.31759977513551,-0.22875851391926,0.742653250546679)) ;
#47707=CARTESIAN_POINT('Ctrl Pts',(1.21068115102719,-0.237766756730124,
0.906564507629634)) ;
#47708=CARTESIAN_POINT('Ctrl Pts',(0.937185311602803,-0.258739597926462,
1.18787810115603)) ;
#47709=CARTESIAN_POINT('Ctrl Pts',(0.772014362866387,-0.269836739712522,
1.30129073030834)) ;
#47710=CARTESIAN_POINT('Ctrl Pts',(0.413990985129278,-0.29131324405455,
1.45433020608324)) ;
#47711=CARTESIAN_POINT('Ctrl Pts',(0.22564585066882,-0.301509802578729,
1.49518297070977)) ;
#47712=CARTESIAN_POINT('Ctrl Pts',(0.0231149140393018,-0.311384174501881,
1.49986648759641)) ;
#47713=CARTESIAN_POINT('Ctrl Pts',(0.0115547705911262,-0.311944070840734,
1.5)) ;
#47714=CARTESIAN_POINT('Ctrl Pts',(1.41550425220223E-14,-0.3125,1.5)) ;
#47715=CARTESIAN_POINT('Ctrl Pts',(4.90915130084568E-14,-0.249999999999995,
1.5)) ;
#47716=CARTESIAN_POINT('Ctrl Pts',(0.0191592501217865,-0.249078200148724,
1.5)) ;
#47717=CARTESIAN_POINT('Ctrl Pts',(0.0383322093844666,-0.248145544213741,
1.49963292591492)) ;
#47718=CARTESIAN_POINT('Ctrl Pts',(0.248674185200841,-0.23780128807632,
1.49156269404616)) ;
#47719=CARTESIAN_POINT('Ctrl Pts',(0.436652034139633,-0.227539515533002,
1.44772606754618)) ;
#47720=CARTESIAN_POINT('Ctrl Pts',(0.792770125914089,-0.205991173594779,
1.28880038621794)) ;
#47721=CARTESIAN_POINT('Ctrl Pts',(0.956362180861738,-0.194891136528308,
1.17254880270888)) ;
#47722=CARTESIAN_POINT('Ctrl Pts',(1.22494646823618,-0.174038182575903,
0.887044092269506)) ;
#47723=CARTESIAN_POINT('Ctrl Pts',(1.32889290290969,-0.165114861284888,
0.722067503127937)) ;
#47724=CARTESIAN_POINT('Ctrl Pts',(1.46860354017829,-0.145080646468042,
0.361451636424709)) ;
#47725=CARTESIAN_POINT('Ctrl Pts',(1.50293052915093,-0.134400071955941,
0.16920129520689)) ;
#47726=CARTESIAN_POINT('Ctrl Pts',(1.49659053880823,-0.112606893140416,
-0.223075923472551)) ;
#47727=CARTESIAN_POINT('Ctrl Pts',(1.45386747113103,-0.101704118359621,
-0.419325869526868)) ;
#47728=CARTESIAN_POINT('Ctrl Pts',(1.29785265196493,-0.0819049369369369,
-0.775711135135183)) ;
#47729=CARTESIAN_POINT('Ctrl Pts',(1.18919831008328,-0.0729433542002783,
-0.933791142129341)) ;
#47730=CARTESIAN_POINT('Ctrl Pts',(0.9146207727033,-0.0522020884534194,
-1.20489446365697)) ;
#47731=CARTESIAN_POINT('Ctrl Pts',(0.749787143876792,-0.0412458924799698,
-1.31381729877768)) ;
#47732=CARTESIAN_POINT('Ctrl Pts',(0.384694175187683,-0.0195251428224716,
-1.4634047151919)) ;
#47733=CARTESIAN_POINT('Ctrl Pts',(0.187586889710424,-0.00906504495717777,
-1.50143159464614)) ;
#47734=CARTESIAN_POINT('Ctrl Pts',(-0.209921866159885,0.0101419464948581,
-1.49848526399372)) ;
#47735=CARTESIAN_POINT('Ctrl Pts',(-0.406427193981676,0.0207347046007646,
-1.45750318392639)) ;
#47736=CARTESIAN_POINT('Ctrl Pts',(-0.768903774840431,0.0424750264145686,
-1.30267945323063)) ;
#47737=CARTESIAN_POINT('Ctrl Pts',(-0.931899884490505,0.0534045251144004,
-1.19153504338665)) ;
#47738=CARTESIAN_POINT('Ctrl Pts',(-1.20251862707306,0.0740614292800871,
-0.916611905055273)) ;
#47739=CARTESIAN_POINT('Ctrl Pts',(-1.30898495960905,0.0829543119014871,
-0.756822385773172)) ;
#47740=CARTESIAN_POINT('Ctrl Pts',(-1.46060335034513,0.10298813736439,-0.396213527440928)) ;
#47741=CARTESIAN_POINT('Ctrl Pts',(-1.50046665242847,0.114038605116938,
-0.197305107895072)) ;
#47742=CARTESIAN_POINT('Ctrl Pts',(-1.4995431543654,0.13592433948451,0.196638110721231)) ;
#47743=CARTESIAN_POINT('Ctrl Pts',(-1.46179849759225,0.146549332465405,
0.387887984377344)) ;
#47744=CARTESIAN_POINT('Ctrl Pts',(-1.31550192893595,0.16646651706018,0.746397307083299)) ;
#47745=CARTESIAN_POINT('Ctrl Pts',(-1.20803649523317,0.175492594998149,
0.910114007074791)) ;
#47746=CARTESIAN_POINT('Ctrl Pts',(-0.933642445954468,0.196487186135895,
1.19065485338835)) ;
#47747=CARTESIAN_POINT('Ctrl Pts',(-0.768187158340748,0.207583488768161,
1.30354478362202)) ;
#47748=CARTESIAN_POINT('Ctrl Pts',(-0.409824740621127,0.229046263369276,
1.45550275424853)) ;
#47749=CARTESIAN_POINT('Ctrl Pts',(-0.221417349171984,0.239230615977489,
1.49580827363276)) ;
#47750=CARTESIAN_POINT('Ctrl Pts',(-0.0203239888607854,0.249019294320898,
1.49989677687175)) ;
#47751=CARTESIAN_POINT('Ctrl Pts',(-0.0101598874830822,0.249511182185562,
1.5)) ;
#47752=CARTESIAN_POINT('Ctrl Pts',(-6.81070803526631E-15,0.250000000000002,
1.5)) ;
#47753=CARTESIAN_POINT('Origin',(0.,1.5,0.)) ;
#47754=CARTESIAN_POINT('',(-1.13659082146001E-13,0.749999999999992,1.5)) ;
#47755=CARTESIAN_POINT('',(-1.2415068972871E-13,0.687499999999986,1.5)) ;
#47756=CARTESIAN_POINT('',(-1.83697019872103E-16,1.5,1.5)) ;
#47757=CARTESIAN_POINT('Ctrl Pts',(-2.48117682437547E-13,0.687499999999986,
1.5)) ;
#47758=CARTESIAN_POINT('Ctrl Pts',(-0.0510614672068272,0.685043304013574,
1.49999999999999)) ;
#47759=CARTESIAN_POINT('Ctrl Pts',(-0.102179477610568,0.682511468087141,
1.49739289784913)) ;
#47760=CARTESIAN_POINT('Ctrl Pts',(-0.344669170413668,0.670153302582107,
1.47250340791462)) ;
#47761=CARTESIAN_POINT('Ctrl Pts',(-0.530592504818994,0.659643040161198,
1.41616262226452)) ;
#47762=CARTESIAN_POINT('Ctrl Pts',(-0.877676886885451,0.637849649816645,
1.23276835411336)) ;
#47763=CARTESIAN_POINT('Ctrl Pts',(-1.0341236120761,0.626768610768905,1.10482462510261)) ;
#47764=CARTESIAN_POINT('Ctrl Pts',(-1.28183875596352,0.606441680690317,
0.802110357290677)) ;
#47765=CARTESIAN_POINT('Ctrl Pts',(-1.37345398630756,0.597641604441125,
0.632548879940103)) ;
#47766=CARTESIAN_POINT('Ctrl Pts',(-1.48927255276646,0.577197970079465,
0.264563461430231)) ;
#47767=CARTESIAN_POINT('Ctrl Pts',(-1.51100291455977,0.566343965788529,
0.0691913841933851)) ;
#47768=CARTESIAN_POINT('Ctrl Pts',(-1.47824767805252,0.544557894761976,
-0.322957894284567)) ;
#47769=CARTESIAN_POINT('Ctrl Pts',(-1.42248125925354,0.533842322046463,
-0.515838203163837)) ;
#47770=CARTESIAN_POINT('Ctrl Pts',(-1.24304955486358,0.51467995777457,-0.860760760057962)) ;
#47771=CARTESIAN_POINT('Ctrl Pts',(-1.12416038075026,0.505166024597211,
-1.01112600981612)) ;
#47772=CARTESIAN_POINT('Ctrl Pts',(-0.8312063682489,0.48404460150766,-1.26408600710638)) ;
#47773=CARTESIAN_POINT('Ctrl Pts',(-0.658165242181626,0.472993280290402,
-1.36221754878023)) ;
#47774=CARTESIAN_POINT('Ctrl Pts',(-0.283470430065135,0.45152259037716,
-1.48617193373867)) ;
#47775=CARTESIAN_POINT('Ctrl Pts',(-0.0854472376909037,0.441903950874523,
-1.5105432744356)) ;
#47776=CARTESIAN_POINT('Ctrl Pts',(0.30305399922152,0.422407069963543,-1.48155944277595)) ;
#47777=CARTESIAN_POINT('Ctrl Pts',(0.489972944982964,0.411999846327852,
-1.43065250284712)) ;
#47778=CARTESIAN_POINT('Ctrl Pts',(0.841192364010326,0.390301777529644,
-1.25785190447179)) ;
#47779=CARTESIAN_POINT('Ctrl Pts',(1.00084972049992,0.379206271374095,-1.13494833611413)) ;
#47780=CARTESIAN_POINT('Ctrl Pts',(1.25769372320449,0.358646139226393,-0.839650441100459)) ;
#47781=CARTESIAN_POINT('Ctrl Pts',(1.35465031011417,0.349839319344135,-0.672107748194327)) ;
#47782=CARTESIAN_POINT('Ctrl Pts',(1.48097046872622,0.329572811631444,-0.30731060936592)) ;
#47783=CARTESIAN_POINT('Ctrl Pts',(1.50827217193254,0.318789518569689,-0.113211334254335)) ;
#47784=CARTESIAN_POINT('Ctrl Pts',(1.48713507777104,0.296988077347213,0.279214607750242)) ;
#47785=CARTESIAN_POINT('Ctrl Pts',(1.43707147471412,0.286184087706954,0.473686421274927)) ;
#47786=CARTESIAN_POINT('Ctrl Pts',(1.26789353267485,0.266738168283495,0.823712970897226)) ;
#47787=CARTESIAN_POINT('Ctrl Pts',(1.15354857632314,0.257515504479239,0.977446581937966)) ;
#47788=CARTESIAN_POINT('Ctrl Pts',(0.868718043953079,0.236559724813284,
1.23851369630045)) ;
#47789=CARTESIAN_POINT('Ctrl Pts',(0.699236785176761,0.225544503037257,
1.34151152910609)) ;
#47790=CARTESIAN_POINT('Ctrl Pts',(0.349606601167749,0.205174756639845,
1.46924515684965)) ;
#47791=CARTESIAN_POINT('Ctrl Pts',(0.175384875096167,0.195938208737378,
1.50000000000001)) ;
#47792=CARTESIAN_POINT('Ctrl Pts',(-9.10382880192628E-14,0.187499999999994,
1.5)) ;
#47793=CARTESIAN_POINT('Ctrl Pts',(-6.97358837342676E-15,0.250000000000002,
1.5)) ;
#47794=CARTESIAN_POINT('Ctrl Pts',(0.188419112446916,0.259065318774311,
1.5)) ;
#47795=CARTESIAN_POINT('Ctrl Pts',(0.375295540662263,0.269042518704381,
1.46450027092331)) ;
#47796=CARTESIAN_POINT('Ctrl Pts',(0.733064149695413,0.290179090100831,
1.32325710884974)) ;
#47797=CARTESIAN_POINT('Ctrl Pts',(0.899468751927728,0.301156645101247,
1.21628635451441)) ;
#47798=CARTESIAN_POINT('Ctrl Pts',(1.17747154217608,0.321970224054261,0.948512469561911)) ;
#47799=CARTESIAN_POINT('Ctrl Pts',(1.28802255728247,0.331005715020445,0.791897129631915)) ;
#47800=CARTESIAN_POINT('Ctrl Pts',(1.44846315974962,0.350687492820267,0.437625129235129)) ;
#47801=CARTESIAN_POINT('Ctrl Pts',(1.49365547206233,0.361558897757654,0.241939840362161)) ;
#47802=CARTESIAN_POINT('Ctrl Pts',(1.5049535533416,0.383358323322134,-0.150449819798485)) ;
#47803=CARTESIAN_POINT('Ctrl Pts',(1.4729717817079,0.394074896368886,-0.343348134640027)) ;
#47804=CARTESIAN_POINT('Ctrl Pts',(1.33775182562377,0.414187860562473,-0.705381490124597)) ;
#47805=CARTESIAN_POINT('Ctrl Pts',(1.23617371768228,0.423058378322597,-0.871217305620668)) ;
#47806=CARTESIAN_POINT('Ctrl Pts',(0.971538021496481,0.443813809003432,
-1.16005033884053)) ;
#47807=CARTESIAN_POINT('Ctrl Pts',(0.80924439776282,0.454914112344198,-1.27856045705693)) ;
#47808=CARTESIAN_POINT('Ctrl Pts',(0.45472027561449,0.476516256240327,-1.44218384524791)) ;
#47809=CARTESIAN_POINT('Ctrl Pts',(0.267070329812062,0.486828586095551,
-1.4884084798686)) ;
#47810=CARTESIAN_POINT('Ctrl Pts',(-0.123236219195116,0.506155635069944,
-1.50815146953946)) ;
#47811=CARTESIAN_POINT('Ctrl Pts',(-0.322301634956137,0.516104922990632,
-1.47846557944368)) ;
#47812=CARTESIAN_POINT('Ctrl Pts',(-0.694584723612933,0.537753336345139,
-1.34393592303366)) ;
#47813=CARTESIAN_POINT('Ctrl Pts',(-0.864478737203401,0.548773170428665,
-1.24148695946718)) ;
#47814=CARTESIAN_POINT('Ctrl Pts',(-1.15023823130796,0.56974809138546,-0.981339767556789)) ;
#47815=CARTESIAN_POINT('Ctrl Pts',(-1.26510100725959,0.579000304066912,
-0.827994526795476)) ;
#47816=CARTESIAN_POINT('Ctrl Pts',(-1.43545918562507,0.598413953974951,
-0.478548828450786)) ;
#47817=CARTESIAN_POINT('Ctrl Pts',(-1.4861801538254,0.609208278114524,-0.284250993938463)) ;
#47818=CARTESIAN_POINT('Ctrl Pts',(-1.50865094126074,0.631008931292407,
0.108160763263435)) ;
#47819=CARTESIAN_POINT('Ctrl Pts',(-1.48198631190391,0.641800785843825,
0.302414145188959)) ;
#47820=CARTESIAN_POINT('Ctrl Pts',(-1.35687171398149,0.662087858154968,
0.667581446789534)) ;
#47821=CARTESIAN_POINT('Ctrl Pts',(-1.26053447779002,0.670890154044406,
0.835355305823441)) ;
#47822=CARTESIAN_POINT('Ctrl Pts',(-1.00474211289518,0.691423661370429,
1.13151619737422)) ;
#47823=CARTESIAN_POINT('Ctrl Pts',(-0.845448042409291,0.702517983983705,
1.2550063880261)) ;
#47824=CARTESIAN_POINT('Ctrl Pts',(-0.494690710056344,0.724227968791487,
1.42903632034362)) ;
#47825=CARTESIAN_POINT('Ctrl Pts',(-0.307878881971955,0.734647510043461,
1.48057222771769)) ;
#47826=CARTESIAN_POINT('Ctrl Pts',(-0.0776203706639568,0.746223695115845,
1.49849544986286)) ;
#47827=CARTESIAN_POINT('Ctrl Pts',(-0.0387892381696761,0.748133751908426,
1.49999999999999)) ;
#47828=CARTESIAN_POINT('Ctrl Pts',(-2.27134467272131E-13,0.749999999999992,
1.5)) ;
#47829=CARTESIAN_POINT('Origin',(0.,1.5,0.)) ;
#47830=CARTESIAN_POINT('',(-6.42610964440854E-14,1.25,1.5)) ;
#47831=CARTESIAN_POINT('',(-1.31145094783846E-14,1.18749999999999,1.5)) ;
#47832=CARTESIAN_POINT('',(-1.83697019872103E-16,1.5,1.5)) ;
#47833=CARTESIAN_POINT('',(0.,1.5,-1.5)) ;
#47834=CARTESIAN_POINT('Ctrl Pts',(-1.28438926161323E-13,1.25,1.5)) ;
#47835=CARTESIAN_POINT('Ctrl Pts',(0.127128967260225,1.25611649528913,1.50000000000001)) ;
#47836=CARTESIAN_POINT('Ctrl Pts',(0.253990145120191,1.26266892091996,1.48384268285135)) ;
#47837=CARTESIAN_POINT('Ctrl Pts',(0.569456085887469,1.28012579796239,1.40179814679003)) ;
#47838=CARTESIAN_POINT('Ctrl Pts',(0.749564711973221,1.29122093510874,1.31433050078366)) ;
#47839=CARTESIAN_POINT('Ctrl Pts',(1.05939698210934,1.31266655119982,1.07893355520466)) ;
#47840=CARTESIAN_POINT('Ctrl Pts',(1.18795943011206,1.32283575506834,0.935518907823889)) ;
#47841=CARTESIAN_POINT('Ctrl Pts',(1.38845165379318,1.34176259152033,0.601415513490284)) ;
#47842=CARTESIAN_POINT('Ctrl Pts',(1.45586730411665,1.35209389722695,0.412309849914715)) ;
#47843=CARTESIAN_POINT('Ctrl Pts',(1.51257980769671,1.37379661020847,0.0216610162474451)) ;
#47844=CARTESIAN_POINT('Ctrl Pts',(1.50248232461383,1.38476864010628,-0.175835521913221)) ;
#47845=CARTESIAN_POINT('Ctrl Pts',(1.40835967583881,1.40556303715002,-0.550134668700435)) ;
#47846=CARTESIAN_POINT('Ctrl Pts',(1.32741330284865,1.41457755125674,-0.723939128419645)) ;
#47847=CARTESIAN_POINT('Ctrl Pts',(1.09974954059502,1.43429063516671,-1.03928494591313)) ;
#47848=CARTESIAN_POINT('Ctrl Pts',(0.952416850700394,1.44517055034509,-1.17577418782125)) ;
#47849=CARTESIAN_POINT('Ctrl Pts',(0.663476955517675,1.46398230579863,-1.35253880535885)) ;
#47850=CARTESIAN_POINT('Ctrl Pts',(0.53453515321281,1.4717401683217,-1.40848810337764)) ;
#47851=CARTESIAN_POINT('Ctrl Pts',(0.269540310930297,1.48652483760024,-1.48175166682828)) ;
#47852=CARTESIAN_POINT('Ctrl Pts',(0.135093550516832,1.49350030852028,-1.5000000000001)) ;
#47853=CARTESIAN_POINT('Ctrl Pts',(-1.11584352868732E-12,1.50000000000006,
-1.5)) ;
#47854=CARTESIAN_POINT('',(-1.05094390383289,1.5,-1.07028823734379)) ;
#47855=CARTESIAN_POINT('Origin',(0.,1.5,0.)) ;
#47856=CARTESIAN_POINT('Ctrl Pts',(-1.05094390383375,1.50000000000005,-1.07028823734295)) ;
#47857=CARTESIAN_POINT('Ctrl Pts',(-0.946934342292571,1.49215890157674,
-1.17241793551985)) ;
#47858=CARTESIAN_POINT('Ctrl Pts',(-0.828604157750759,1.48406532833449,
-1.25883268054643)) ;
#47859=CARTESIAN_POINT('Ctrl Pts',(-0.571466074106988,1.4679271682902,-1.394430216709)) ;
#47860=CARTESIAN_POINT('Ctrl Pts',(-0.434119963984296,1.45996699073399,
-1.44310616777797)) ;
#47861=CARTESIAN_POINT('Ctrl Pts',(-0.103631625899206,1.44224491368682,
-1.50867834860404)) ;
#47862=CARTESIAN_POINT('Ctrl Pts',(0.0900562705017904,1.43343242685769,
-1.50954940292535)) ;
#47863=CARTESIAN_POINT('Ctrl Pts',(0.469431154236831,1.41318722380876,-1.43781866690835)) ;
#47864=CARTESIAN_POINT('Ctrl Pts',(0.651366029083658,1.40241290333334,-1.36506357669648)) ;
#47865=CARTESIAN_POINT('Ctrl Pts',(0.981346300335995,1.38061091365567,-1.15173454360488)) ;
#47866=CARTESIAN_POINT('Ctrl Pts',(1.125225928,1.36979706333053,-1.01164275718773)) ;
#47867=CARTESIAN_POINT('Ctrl Pts',(1.34489832416677,1.35031785689487,-0.690875076685086)) ;
#47868=CARTESIAN_POINT('Ctrl Pts',(1.42147844966884,1.34112468997402,-0.515244419531858)) ;
#47869=CARTESIAN_POINT('Ctrl Pts',(1.50645493676708,1.3201887338785,-0.138397209812553)) ;
#47870=CARTESIAN_POINT('Ctrl Pts',(1.51161612816481,1.30917840593553,0.0597886931608237)) ;
#47871=CARTESIAN_POINT('Ctrl Pts',(1.44470672617466,1.28748460512355,0.450277107776453)) ;
#47872=CARTESIAN_POINT('Ctrl Pts',(1.37195785681797,1.2774401639486,0.638454811703191)) ;
#47873=CARTESIAN_POINT('Ctrl Pts',(1.16156209292362,1.2581578519111,0.968201892290707)) ;
#47874=CARTESIAN_POINT('Ctrl Pts',(1.02867313929654,1.24787108496626,1.10835508285814)) ;
#47875=CARTESIAN_POINT('Ctrl Pts',(0.711369794242329,1.22629592738095,1.33547524088418)) ;
#47876=CARTESIAN_POINT('Ctrl Pts',(0.528252383420287,1.21519553135519,1.41792083851705)) ;
#47877=CARTESIAN_POINT('Ctrl Pts',(0.224436492138917,1.19864829653047,1.48739673236104)) ;
#47878=CARTESIAN_POINT('Ctrl Pts',(0.112278148308194,1.19290198492915,1.5)) ;
#47879=CARTESIAN_POINT('Ctrl Pts',(-2.61943244872498E-14,1.18749999999999,
1.5)) ;
#47880=CARTESIAN_POINT('Origin',(0.,1.5,0.)) ;
#47881=CARTESIAN_POINT('',(1.69915517524252E-11,1.1830127018909,-1.1830127018909)) ;
#47882=CARTESIAN_POINT('',(9.7613887853463E-10,1.35212341201692,-1.35212341201692)) ;
#47883=CARTESIAN_POINT('',(-1.83697019872103E-16,1.5,-1.5)) ;
#47884=CARTESIAN_POINT('Ctrl Pts',(0.190653686730815,1.17524047357919,-1.15967294634072)) ;
#47885=CARTESIAN_POINT('Ctrl Pts',(0.122204175781398,1.17817852967127,-1.17390374658709)) ;
#47886=CARTESIAN_POINT('Ctrl Pts',(0.0581138399920893,1.18076514130866,
-1.18076514130699)) ;
#47887=CARTESIAN_POINT('Ctrl Pts',(3.39832483821223E-11,1.1830127018909,
-1.1830127018909)) ;
#47888=CARTESIAN_POINT('Ctrl Pts',(0.943477955795641,1.17524047358084,-0.700742119235161)) ;
#47889=CARTESIAN_POINT('Ctrl Pts',(0.87639271171186,1.19709475518657,-0.827718196131212)) ;
#47890=CARTESIAN_POINT('Ctrl Pts',(0.787836640815196,1.21979792390211,-0.941972631438311)) ;
#47891=CARTESIAN_POINT('Ctrl Pts',(0.567629405650076,1.26638165677038,-1.14223242554796)) ;
#47892=CARTESIAN_POINT('Ctrl Pts',(0.43515803729191,1.28984247119423,-1.22380807368022)) ;
#47893=CARTESIAN_POINT('Ctrl Pts',(0.186827921684265,1.32764663045991,-1.31906224930678)) ;
#47894=CARTESIAN_POINT('Ctrl Pts',(0.0879972129962622,1.34101066661199,
-1.34101066648493)) ;
#47895=CARTESIAN_POINT('Ctrl Pts',(1.95227783592045E-9,1.35212341201693,
-1.35212341201692)) ;
#47896=CARTESIAN_POINT('Origin',(0.,-1.5,0.)) ;
#47897=CARTESIAN_POINT('',(5.8487450577825E-15,-1.22263611415569,-1.22263611415569)) ;
#47898=CARTESIAN_POINT('',(1.83697019872103E-16,-1.5,-1.5)) ;
#47899=CARTESIAN_POINT('Ctrl Pts',(-0.943477955795637,-1.17524047358084,
-0.700742119235167)) ;
#47900=CARTESIAN_POINT('Ctrl Pts',(-0.856400153191489,-1.18162007517788,
-0.828682984693854)) ;
#47901=CARTESIAN_POINT('Ctrl Pts',(-0.74531176971572,-1.18842626255131,
-0.938491399735298)) ;
#47902=CARTESIAN_POINT('Ctrl Pts',(-0.49287562585092,-1.20180300792309,
-1.10604526103621)) ;
#47903=CARTESIAN_POINT('Ctrl Pts',(-0.355181554475564,-1.20825650987825,
-1.16433423964103)) ;
#47904=CARTESIAN_POINT('Ctrl Pts',(-0.141096246039747,-1.21720626328448,
-1.21107258328805)) ;
#47905=CARTESIAN_POINT('Ctrl Pts',(-0.071499869986318,-1.21996046433649,
-1.21996046433649)) ;
#47906=CARTESIAN_POINT('Ctrl Pts',(1.15477603751927E-14,-1.22263611415569,
-1.22263611415569)) ;
#47907=CARTESIAN_POINT('Ctrl Pts',(0.,-1.49999999999999,-1.49999999999999)) ;
#47908=CARTESIAN_POINT('Ctrl Pts',(-0.054521208291996,-1.49379355370233,
-1.49379355370233)) ;
#47909=CARTESIAN_POINT('Ctrl Pts',(-0.155386697464455,-1.4820996664401,
-1.47945377533922)) ;
#47910=CARTESIAN_POINT('Ctrl Pts',(-0.360512792586367,-1.45487588361295,
-1.41215042182259)) ;
#47911=CARTESIAN_POINT('Ctrl Pts',(-0.440541053484735,-1.44346315326101,
-1.37729805085287)) ;
#47912=CARTESIAN_POINT('Ctrl Pts',(-0.660564421494151,-1.40957426184176,
-1.25580759883132)) ;
#47913=CARTESIAN_POINT('Ctrl Pts',(-0.789067667032358,-1.38650470000743,
-1.15160047641225)) ;
#47914=CARTESIAN_POINT('Ctrl Pts',(-1.02696295019047,-1.33537286947486,
-0.87618009528097)) ;
#47915=CARTESIAN_POINT('Ctrl Pts',(-1.09540172650555,-1.31417335514527,
-0.731932035287483)) ;
#47916=CARTESIAN_POINT('Ctrl Pts',(-1.18503213710912,-1.28327672009811,
-0.512590967679951)) ;
#47917=CARTESIAN_POINT('Ctrl Pts',(-1.21503192269102,-1.26261772581496,
-0.371319335995457)) ;
#47918=CARTESIAN_POINT('Ctrl Pts',(-1.22344776915413,-1.2195157042751,-0.092198866685286)) ;
#47919=CARTESIAN_POINT('Ctrl Pts',(-1.20421128370105,-1.1975036728211,0.0434683361937809)) ;
#47920=CARTESIAN_POINT('Ctrl Pts',(-1.16245326511947,-1.17524047358084,
0.172894699616844)) ;
#47921=CARTESIAN_POINT('Origin',(0.,-1.5,0.)) ;
#47922=CARTESIAN_POINT('Origin',(0.,-1.5,0.)) ;
#47923=CARTESIAN_POINT('Ctrl Pts',(1.15477603751927E-14,-1.22263611415569,
-1.22263611415569)) ;
#47924=CARTESIAN_POINT('Ctrl Pts',(0.00763880650807998,-1.22292197161608,
-1.22292197161608)) ;
#47925=CARTESIAN_POINT('Ctrl Pts',(0.0152991705677857,-1.22320998165175,
-1.2231384112653)) ;
#47926=CARTESIAN_POINT('Ctrl Pts',(0.188113702875513,-1.22973789977246,
-1.22642064958551)) ;
#47927=CARTESIAN_POINT('Ctrl Pts',(0.352214880870685,-1.23655764082388,
-1.19676195776366)) ;
#47928=CARTESIAN_POINT('Ctrl Pts',(0.65186654613245,-1.25016075841606,-1.07824422992583)) ;
#47929=CARTESIAN_POINT('Ctrl Pts',(0.785743879428164,-1.25680894903653,
-0.993389073013124)) ;
#47930=CARTESIAN_POINT('Ctrl Pts',(1.05115350497959,-1.27146311884125,-0.744547013637275)) ;
#47931=CARTESIAN_POINT('Ctrl Pts',(1.13835376715091,-1.27738305068912,-0.592802361635772)) ;
#47932=CARTESIAN_POINT('Ctrl Pts',(1.25967765756574,-1.28872257112954,-0.321841073898619)) ;
#47933=CARTESIAN_POINT('Ctrl Pts',(1.29814354148902,-1.29570591263743,-0.152413792331758)) ;
#47934=CARTESIAN_POINT('Ctrl Pts',(1.30662190456781,-1.30918043223515,0.18003450505882)) ;
#47935=CARTESIAN_POINT('Ctrl Pts',(1.28098182378621,-1.31555878519823,0.339873491658122)) ;
#47936=CARTESIAN_POINT('Ctrl Pts',(1.19729600860591,-1.32477289663106,0.573777581337942)) ;
#47937=CARTESIAN_POINT('Ctrl Pts',(1.1595090993149,-1.32775228607298,0.652757041424446)) ;
#47938=CARTESIAN_POINT('Ctrl Pts',(1.0217351705496,-1.33718906902534,0.881033282308611)) ;
#47939=CARTESIAN_POINT('Ctrl Pts',(0.89957409461852,-1.34406809219364,1.01457191343034)) ;
#47940=CARTESIAN_POINT('Ctrl Pts',(0.618226364819832,-1.35765968699375,
1.22053654692002)) ;
#47941=CARTESIAN_POINT('Ctrl Pts',(0.463899970012846,-1.36424162041716,
1.29407692709582)) ;
#47942=CARTESIAN_POINT('Ctrl Pts',(0.0787412807004137,-1.3788865771125,
1.3954971876506)) ;
#47943=CARTESIAN_POINT('Ctrl Pts',(-0.112750685838222,-1.38484130930519,
1.38637264346196)) ;
#47944=CARTESIAN_POINT('Ctrl Pts',(-0.424963139540061,-1.39609957847364,
1.34263453098656)) ;
#47945=CARTESIAN_POINT('Ctrl Pts',(-0.601276957302403,-1.40306739103552,
1.2811021788905)) ;
#47946=CARTESIAN_POINT('Ctrl Pts',(-0.920932661732956,-1.41694406395078,
1.09278570715895)) ;
#47947=CARTESIAN_POINT('Ctrl Pts',(-1.06092241118538,-1.42371641827071,
0.967470185148511)) ;
#47948=CARTESIAN_POINT('Ctrl Pts',(-1.22864359259982,-1.43307254901287,
0.743570357888767)) ;
#47949=CARTESIAN_POINT('Ctrl Pts',(-1.27714358218595,-1.43599236885225,
0.662964068257706)) ;
#47950=CARTESIAN_POINT('Ctrl Pts',(-1.39572498250574,-1.44518361825711,
0.41630053272665)) ;
#47951=CARTESIAN_POINT('Ctrl Pts',(-1.44314086925414,-1.45167913699272,
0.239798991761196)) ;
#47952=CARTESIAN_POINT('Ctrl Pts',(-1.47198220396756,-1.46528635709641,
-0.135232180635479)) ;
#47953=CARTESIAN_POINT('Ctrl Pts',(-1.44783342734718,-1.47227055818032,
-0.330648659022112)) ;
#47954=CARTESIAN_POINT('Ctrl Pts',(-1.35080505786766,-1.48251153393605,
-0.620873502013194)) ;
#47955=CARTESIAN_POINT('Ctrl Pts',(-1.30387790518947,-1.48588700190698,
-0.721113686459145)) ;
#47956=CARTESIAN_POINT('Ctrl Pts',(-1.19033775786212,-1.49278551889176,
-0.90719521171022)) ;
#47957=CARTESIAN_POINT('Ctrl Pts',(-1.12488215104792,-1.49634374468731,
-0.992562134937736)) ;
#47958=CARTESIAN_POINT('Ctrl Pts',(-1.05094390383307,-1.5,-1.07028823734362)) ;
#47959=CARTESIAN_POINT('Origin',(0.,1.5,0.)) ;
#47960=CARTESIAN_POINT('Ctrl Pts',(1.95227807856166E-9,1.35212341201693,
-1.35212341201692)) ;
#47961=CARTESIAN_POINT('Ctrl Pts',(-0.088090331159446,1.36324791734227,
-1.36324791746946)) ;
#47962=CARTESIAN_POINT('Ctrl Pts',(-0.165022923254981,1.37330834159026,
-1.36467558293643)) ;
#47963=CARTESIAN_POINT('Ctrl Pts',(-0.372223984929874,1.40076164095228,
-1.35821753696589)) ;
#47964=CARTESIAN_POINT('Ctrl Pts',(-0.517313736874783,1.42078762161895,
-1.33122592552885)) ;
#47965=CARTESIAN_POINT('Ctrl Pts',(-0.797750176409724,1.46102555179597,
-1.2330414343537)) ;
#47966=CARTESIAN_POINT('Ctrl Pts',(-0.931055473779404,1.48099102241791,
-1.16136888733187)) ;
#47967=CARTESIAN_POINT('Ctrl Pts',(-1.05094390383392,1.50000000000013,-1.07028823734296)) ;
#47968=CARTESIAN_POINT('Origin',(0.,1.5,0.)) ;
#47969=CARTESIAN_POINT('Ctrl Pts',(3.39832483821223E-11,1.1830127018909,
-1.1830127018909)) ;
#47970=CARTESIAN_POINT('Ctrl Pts',(-0.0881364884218503,1.1864213924446,
-1.18642139244713)) ;
#47971=CARTESIAN_POINT('Ctrl Pts',(-0.162469886569823,1.1894852589927,-1.17963706679332)) ;
#47972=CARTESIAN_POINT('Ctrl Pts',(-0.344721916499354,1.19717151895269,
-1.15365394859358)) ;
#47973=CARTESIAN_POINT('Ctrl Pts',(-0.468394433977734,1.20277853643706,
-1.11526159830785)) ;
#47974=CARTESIAN_POINT('Ctrl Pts',(-0.717977954481682,1.21494469994253,
-0.991479164438509)) ;
#47975=CARTESIAN_POINT('Ctrl Pts',(-0.838726254773585,1.22140244274215,
-0.900448279090885)) ;
#47976=CARTESIAN_POINT('Ctrl Pts',(-0.993074931050609,1.23066292138297,
-0.731155613055594)) ;
#47977=CARTESIAN_POINT('Ctrl Pts',(-1.03996298568237,1.23364082281887,-0.668434677590451)) ;
#47978=CARTESIAN_POINT('Ctrl Pts',(-1.16787199372824,1.24287513018846,-0.456760585322658)) ;
#47979=CARTESIAN_POINT('Ctrl Pts',(-1.22498602286769,1.24969109010067,-0.298218403352094)) ;
#47980=CARTESIAN_POINT('Ctrl Pts',(-1.27299648961919,1.26329436412094,0.0239120303898897)) ;
#47981=CARTESIAN_POINT('Ctrl Pts',(-1.26652670310226,1.26994623938014,0.184012297019625)) ;
#47982=CARTESIAN_POINT('Ctrl Pts',(-1.18346232080173,1.28455636029785,0.540836393778874)) ;
#47983=CARTESIAN_POINT('Ctrl Pts',(-1.09549431485504,1.29047203254427,0.69388259441924)) ;
#47984=CARTESIAN_POINT('Ctrl Pts',(-0.919018352996627,1.30186467240575,
0.938319739625856)) ;
#47985=CARTESIAN_POINT('Ctrl Pts',(-0.790286241919958,1.30884866284902,
1.05769021139879)) ;
#47986=CARTESIAN_POINT('Ctrl Pts',(-0.503791478080934,1.3223282587274,1.23329014532573)) ;
#47987=CARTESIAN_POINT('Ctrl Pts',(-0.35101607093844,1.32871063087591,1.29171656762766)) ;
#47988=CARTESIAN_POINT('Ctrl Pts',(0.00224632758886806,1.34190441912239,
1.35625398851413)) ;
#47989=CARTESIAN_POINT('Ctrl Pts',(0.184090354887929,1.34784528749819,1.34460482878569)) ;
#47990=CARTESIAN_POINT('Ctrl Pts',(0.509771235001103,1.36037444892477,1.27326893451926)) ;
#47991=CARTESIAN_POINT('Ctrl Pts',(0.671642444484427,1.36717720200835,1.20354849922269)) ;
#47992=CARTESIAN_POINT('Ctrl Pts',(0.965216569005918,1.3807389647173,1.00366016750726)) ;
#47993=CARTESIAN_POINT('Ctrl Pts',(1.09284305366252,1.38735662928258,0.873505715555011)) ;
#47994=CARTESIAN_POINT('Ctrl Pts',(1.24736640638551,1.39674825266539,0.636722907990449)) ;
#47995=CARTESIAN_POINT('Ctrl Pts',(1.33749441009985,1.40274261027107,0.479517003122467)) ;
#47996=CARTESIAN_POINT('Ctrl Pts',(1.42759692443734,1.41784814293474,0.0788339234383507)) ;
#47997=CARTESIAN_POINT('Ctrl Pts',(1.43262059128626,1.42476051709303,-0.107230746119766)) ;
#47998=CARTESIAN_POINT('Ctrl Pts',(1.38677319302375,1.43471221787533,-0.378874130966391)) ;
#47999=CARTESIAN_POINT('Ctrl Pts',(1.36300563214594,1.43791909864246,-0.467028878906141)) ;
#48000=CARTESIAN_POINT('Ctrl Pts',(1.25904594518336,1.44792023136461,-0.743648780311062)) ;
#48001=CARTESIAN_POINT('Ctrl Pts',(1.15202715535141,1.45375905173618,-0.902957154604828)) ;
#48002=CARTESIAN_POINT('Ctrl Pts',(0.90829713609045,1.46628394022629,-1.16634790760792)) ;
#48003=CARTESIAN_POINT('Ctrl Pts',(0.755164312600782,1.47308966663899,-1.2787102515016)) ;
#48004=CARTESIAN_POINT('Ctrl Pts',(0.4969372415121,1.48321248126175,-1.40087759364243)) ;
#48005=CARTESIAN_POINT('Ctrl Pts',(0.404922654524661,1.48660505005347,-1.43370843375369)) ;
#48006=CARTESIAN_POINT('Ctrl Pts',(0.208709632125688,1.49342040871883,-1.48246367972118)) ;
#48007=CARTESIAN_POINT('Ctrl Pts',(0.104681834995791,1.49680698242307,-1.49680698242307)) ;
#48008=CARTESIAN_POINT('Ctrl Pts',(2.33493779866478E-14,1.5,-1.5)) ;
#48009=CARTESIAN_POINT('Origin',(0.,1.5,0.)) ;
#48010=CARTESIAN_POINT('Ctrl Pts',(-2.6045321936897E-14,1.18749999999999,
1.5)) ;
#48011=CARTESIAN_POINT('Ctrl Pts',(-0.0798363712549382,1.18365887079706,
1.5)) ;
#48012=CARTESIAN_POINT('Ctrl Pts',(-0.159716095570403,1.1796386315509,1.49362712814615)) ;
#48013=CARTESIAN_POINT('Ctrl Pts',(-0.43003397416229,1.165421652833,1.45002019421712)) ;
#48014=CARTESIAN_POINT('Ctrl Pts',(-0.613395332234769,1.15472324803505,
1.38246880981732)) ;
#48015=CARTESIAN_POINT('Ctrl Pts',(-0.948787731355424,1.13292657122318,
1.17870512033934)) ;
#48016=CARTESIAN_POINT('Ctrl Pts',(-1.096542244985,1.12203894221217,1.04266880059696)) ;
#48017=CARTESIAN_POINT('Ctrl Pts',(-1.32519419631909,1.10229714159564,0.728000775362096)) ;
#48018=CARTESIAN_POINT('Ctrl Pts',(-1.40668218866386,1.09330106024026,0.554419084324286)) ;
#48019=CARTESIAN_POINT('Ctrl Pts',(-1.50192885849926,1.07252432270249,0.180437808644521)) ;
#48020=CARTESIAN_POINT('Ctrl Pts',(-1.51263201628805,1.06155746974118,-0.0169655446590038)) ;
#48021=CARTESIAN_POINT('Ctrl Pts',(-1.45715689112896,1.03984854017038,-0.407726276933393)) ;
#48022=CARTESIAN_POINT('Ctrl Pts',(-1.39033878469355,1.02947503072142,-0.597036308852029)) ;
#48023=CARTESIAN_POINT('Ctrl Pts',(-1.19093892832266,1.01058488791976,-0.931710767455425)) ;
#48024=CARTESIAN_POINT('Ctrl Pts',(-1.06287946255845,1.00042968985607,-1.07549239665475)) ;
#48025=CARTESIAN_POINT('Ctrl Pts',(-0.753920534884024,0.97900005206253,
-1.31182679703802)) ;
#48026=CARTESIAN_POINT('Ctrl Pts',(-0.574166690500253,0.967906112079596,
-1.39986584509514)) ;
#48027=CARTESIAN_POINT('Ctrl Pts',(-0.194540542660304,0.946860401386108,
-1.49997965412028)) ;
#48028=CARTESIAN_POINT('Ctrl Pts',(0.0012248453091426,0.937789401646168,
-1.51253995356844)) ;
#48029=CARTESIAN_POINT('Ctrl Pts',(0.385378877770893,0.917915273631611,
-1.46244564720063)) ;
#48030=CARTESIAN_POINT('Ctrl Pts',(0.570169026992564,0.907311327584705,
-1.40076951670215)) ;
#48031=CARTESIAN_POINT('Ctrl Pts',(0.912876418247017,0.885441247393907,
-1.20703324361547)) ;
#48032=CARTESIAN_POINT('Ctrl Pts',(1.0660107708773,0.874383822393379,-1.07420242273627)) ;
#48033=CARTESIAN_POINT('Ctrl Pts',(1.30465774113417,0.854293103028418,-0.76428520315489)) ;
#48034=CARTESIAN_POINT('Ctrl Pts',(1.39104230863307,0.84542671616715,-0.592680891008473)) ;
#48035=CARTESIAN_POINT('Ctrl Pts',(1.49634230880408,0.824810437592514,-0.221587876665044)) ;
#48036=CARTESIAN_POINT('Ctrl Pts',(1.51244984009989,0.813894455278159,-0.0251001950066589)) ;
#48037=CARTESIAN_POINT('Ctrl Pts',(1.46807171896181,0.792143001247831,0.366425977539252)) ;
#48038=CARTESIAN_POINT('Ctrl Pts',(1.40665379793001,0.781525406973956,0.557542674469026)) ;
#48039=CARTESIAN_POINT('Ctrl Pts',(1.2170138822344,0.762652401431149,0.897256774239602)) ;
#48040=CARTESIAN_POINT('Ctrl Pts',(1.09349182081601,0.752769599104504,1.04427782355261)) ;
#48041=CARTESIAN_POINT('Ctrl Pts',(0.792333292811163,0.731485057323399,
1.28889945603531)) ;
#48042=CARTESIAN_POINT('Ctrl Pts',(0.615815035989745,0.720407146400333,
1.38196565998746)) ;
#48043=CARTESIAN_POINT('Ctrl Pts',(0.287670719484251,0.701917111808417,
1.47924427689397)) ;
#48044=CARTESIAN_POINT('Ctrl Pts',(0.144088320348377,0.694432452545015,
1.50000000000002)) ;
#48045=CARTESIAN_POINT('Ctrl Pts',(-2.47926679186605E-13,0.687499999999986,
1.5)) ;
#48046=CARTESIAN_POINT('Ctrl Pts',(-2.2735285876152E-13,0.749999999999992,
1.5)) ;
#48047=CARTESIAN_POINT('Ctrl Pts',(0.158006103608433,0.75760207220433,1.50000000000002)) ;
#48048=CARTESIAN_POINT('Ctrl Pts',(0.315250620966226,0.765860831423893,
1.47504016137086)) ;
#48049=CARTESIAN_POINT('Ctrl Pts',(0.653267439396651,0.78519192030018,1.36458326515879)) ;
#48050=CARTESIAN_POINT('Ctrl Pts',(0.82672058281258,0.796246860045977,1.26703509143898)) ;
#48051=CARTESIAN_POINT('Ctrl Pts',(1.12063201557542,0.817387540584502,1.01504012652266)) ;
#48052=CARTESIAN_POINT('Ctrl Pts',(1.24005937638741,0.826940670742474,0.865067926635356)) ;
#48053=CARTESIAN_POINT('Ctrl Pts',(1.42068979071896,0.84606941821889,0.520750472059851)) ;
#48054=CARTESIAN_POINT('Ctrl Pts',(1.47712141321613,0.856773999403544,0.328068010736083)) ;
#48055=CARTESIAN_POINT('Ctrl Pts',(1.51123898851943,0.878557009171926,-0.0640261650948025)) ;
#48056=CARTESIAN_POINT('Ctrl Pts',(1.49016513143508,0.889418731933562,-0.259537174804263)) ;
#48057=CARTESIAN_POINT('Ctrl Pts',(1.37557842161795,0.909882833718419,-0.627891006931695)) ;
#48058=CARTESIAN_POINT('Ctrl Pts',(1.28458176657173,0.918686934078499,-0.797690513005034)) ;
#48059=CARTESIAN_POINT('Ctrl Pts',(1.03793264536063,0.938986325811679,-1.10125980581968)) ;
#48060=CARTESIAN_POINT('Ctrl Pts',(0.88186907475974,0.950065062357037,-1.22978428796118)) ;
#48061=CARTESIAN_POINT('Ctrl Pts',(0.535285523623325,0.97186839266754,-1.41440385950336)) ;
#48062=CARTESIAN_POINT('Ctrl Pts',(0.349488035948599,0.982390114957565,
-1.47137517337296)) ;
#48063=CARTESIAN_POINT('Ctrl Pts',(-0.0365994568080561,1.00210159403079,
-1.51226526638763)) ;
#48064=CARTESIAN_POINT('Ctrl Pts',(-0.233325040066266,1.01137560495447,
-1.49460904571161)) ;
#48065=CARTESIAN_POINT('Ctrl Pts',(-0.610896023456313,1.03260960557388,
-1.38415715010836)) ;
#48066=CARTESIAN_POINT('Ctrl Pts',(-0.787805789672123,1.04368992503295,
-1.2916823530226)) ;
#48067=CARTESIAN_POINT('Ctrl Pts',(-1.08990680135838,1.06499292132518,-1.04802878776064)) ;
#48068=CARTESIAN_POINT('Ctrl Pts',(-1.21396431585872,1.07492285292586,-0.901388647334283)) ;
#48069=CARTESIAN_POINT('Ctrl Pts',(-1.40476782507156,1.09376243663884,-0.562276140500701)) ;
#48070=CARTESIAN_POINT('Ctrl Pts',(-1.46682776544324,1.10436823503014,-0.371371769457348)) ;
#48071=CARTESIAN_POINT('Ctrl Pts',(-1.51253331375705,1.12611450906356,0.0200611631441543)) ;
#48072=CARTESIAN_POINT('Ctrl Pts',(-1.49707111289976,1.13703701072081,0.216666192974721)) ;
#48073=CARTESIAN_POINT('Ctrl Pts',(-1.39297412284888,1.15767272633219,0.588109073979515)) ;
#48074=CARTESIAN_POINT('Ctrl Pts',(-1.30718060273184,1.1665512616293,0.759948637254943)) ;
#48075=CARTESIAN_POINT('Ctrl Pts',(-1.06956567425292,1.18661482367153,1.07067574201322)) ;
#48076=CARTESIAN_POINT('Ctrl Pts',(-0.916815781785327,1.19766898747329,
1.20405506427194)) ;
#48077=CARTESIAN_POINT('Ctrl Pts',(-0.574623050279518,1.21954667255649,
1.39895653031842)) ;
#48078=CARTESIAN_POINT('Ctrl Pts',(-0.389970772161892,1.2301607365114,1.46123570526209)) ;
#48079=CARTESIAN_POINT('Ctrl Pts',(-0.132606832253855,1.24349796140355,
1.49560838142262)) ;
#48080=CARTESIAN_POINT('Ctrl Pts',(-0.0662729511061171,1.24681144115324,
1.49999999999999)) ;
#48081=CARTESIAN_POINT('Ctrl Pts',(-1.28338495868299E-13,1.25,1.5)) ;
#48082=CARTESIAN_POINT('Origin',(3.46944695195362E-16,1.71875,2.77555756156289E-16)) ;
#48083=CARTESIAN_POINT('Ctrl Pts',(-5.38273142618428E-13,0.93749999999997,
1.17524047358083)) ;
#48084=CARTESIAN_POINT('Ctrl Pts',(-0.0372628755316404,0.935211773494173,
1.17524047358081)) ;
#48085=CARTESIAN_POINT('Ctrl Pts',(-0.0745659590150219,0.932858250931482,
1.1734683901451)) ;
#48086=CARTESIAN_POINT('Ctrl Pts',(-0.261993141982916,0.920713849671594,
1.15555958845237)) ;
#48087=CARTESIAN_POINT('Ctrl Pts',(-0.408006918246224,0.910217893515267,
1.11241632793315)) ;
#48088=CARTESIAN_POINT('Ctrl Pts',(-0.680959750452341,0.888428495475987,
0.970597722086583)) ;
#48089=CARTESIAN_POINT('Ctrl Pts',(-0.804232669945397,0.877334580368952,
0.871200248783751)) ;
#48090=CARTESIAN_POINT('Ctrl Pts',(-1.00011814589685,0.856937259941698,
0.63516168914757)) ;
#48091=CARTESIAN_POINT('Ctrl Pts',(-1.07288678901601,0.848136373379309,
0.50257569992399)) ;
#48092=CARTESIAN_POINT('Ctrl Pts',(-1.16553188026456,0.827712242222803,
0.214536513049786)) ;
#48093=CARTESIAN_POINT('Ctrl Pts',(-1.18351018505052,0.816861997968989,
0.0615167587059378)) ;
#48094=CARTESIAN_POINT('Ctrl Pts',(-1.15971835407239,0.795053447968922,
-0.246046728856358)) ;
#48095=CARTESIAN_POINT('Ctrl Pts',(-1.11689632394281,0.784310216512354,
-0.397557293954039)) ;
#48096=CARTESIAN_POINT('Ctrl Pts',(-0.977772301015633,0.765075235042987,
-0.668826038730583)) ;
#48097=CARTESIAN_POINT('Ctrl Pts',(-0.885233845820656,0.755616003331456,
-0.787246054793336)) ;
#48098=CARTESIAN_POINT('Ctrl Pts',(-0.656668880959004,0.734504563011645,
-0.986824381689021)) ;
#48099=CARTESIAN_POINT('Ctrl Pts',(-0.521463213671476,0.723448798493307,
-1.06447766275569)) ;
#48100=CARTESIAN_POINT('Ctrl Pts',(-0.228029199857764,0.701925845536696,
-1.16330653237555)) ;
#48101=CARTESIAN_POINT('Ctrl Pts',(-0.072637477112143,0.692242977263605,
-1.18320800497987)) ;
#48102=CARTESIAN_POINT('Ctrl Pts',(0.232265954968764,0.672762373986269,
-1.16185079863502)) ;
#48103=CARTESIAN_POINT('Ctrl Pts',(0.378967024087167,0.662361862018095,
-1.12259004120972)) ;
#48104=CARTESIAN_POINT('Ctrl Pts',(0.654832807433886,0.64066215361674,-0.988346580159853)) ;
#48105=CARTESIAN_POINT('Ctrl Pts',(0.780380539295739,0.629556355256246,
-0.892554021127282)) ;
#48106=CARTESIAN_POINT('Ctrl Pts',(0.982771364807177,0.608947755585498,
-0.661823763413569)) ;
#48107=CARTESIAN_POINT('Ctrl Pts',(1.05935465762482,0.600128932644653,-0.530676535459642)) ;
#48108=CARTESIAN_POINT('Ctrl Pts',(1.15947644658547,0.579866759244312,-0.244921420306135)) ;
#48109=CARTESIAN_POINT('Ctrl Pts',(1.18141591408789,0.569082068675803,-0.0928261620922505)) ;
#48110=CARTESIAN_POINT('Ctrl Pts',(1.16589585188604,0.547262074423877,0.214898722445718)) ;
#48111=CARTESIAN_POINT('Ctrl Pts',(1.12713807580175,0.536439614695771,0.367526634799766)) ;
#48112=CARTESIAN_POINT('Ctrl Pts',(0.995315864577872,0.51694735128298,0.642423797412707)) ;
#48113=CARTESIAN_POINT('Ctrl Pts',(0.906006071567535,0.507742733730941,
0.763238533768287)) ;
#48114=CARTESIAN_POINT('Ctrl Pts',(0.683219861600841,0.48678232321035,0.968566045760291)) ;
#48115=CARTESIAN_POINT('Ctrl Pts',(0.550553352182226,0.475760290415287,
1.04966584798988)) ;
#48116=CARTESIAN_POINT('Ctrl Pts',(0.275839516173969,0.455305018730002,
1.15080424286477)) ;
#48117=CARTESIAN_POINT('Ctrl Pts',(0.138388810772653,0.445998134950735,
1.17524047358085)) ;
#48118=CARTESIAN_POINT('Ctrl Pts',(-1.67053870736567E-13,0.437499999999993,
1.17524047358083)) ;
#48119=CARTESIAN_POINT('Ctrl Pts',(-3.7771868965919E-13,0.499999999999977,
1.17524047358083)) ;
#48120=CARTESIAN_POINT('Ctrl Pts',(0.129223051317171,0.507935286983878,
1.17524047358087)) ;
#48121=CARTESIAN_POINT('Ctrl Pts',(0.257722867946538,0.516581478161535,
1.15393619320277)) ;
#48122=CARTESIAN_POINT('Ctrl Pts',(0.526404828087052,0.536338948242251,
1.06203231537727)) ;
#48123=CARTESIAN_POINT('Ctrl Pts',(0.661187746072155,0.547389584135236,
0.983791467874058)) ;
#48124=CARTESIAN_POINT('Ctrl Pts',(0.88877885643814,0.568475796884882,0.783237938588865)) ;
#48125=CARTESIAN_POINT('Ctrl Pts',(0.980771591358329,0.577887854325915,
0.664417204720868)) ;
#48126=CARTESIAN_POINT('Ctrl Pts',(1.11867208140571,0.597166381725078,0.392534336674487)) ;
#48127=CARTESIAN_POINT('Ctrl Pts',(1.16081391242959,0.607923470814767,0.240828338961106)) ;
#48128=CARTESIAN_POINT('Ctrl Pts',(1.1832164248039,0.629735054227077,-0.0667779284672581)) ;
#48129=CARTESIAN_POINT('Ctrl Pts',(1.16457058127801,0.640574794194408,-0.219649542059652)) ;
#48130=CARTESIAN_POINT('Ctrl Pts',(1.07066961934905,0.660971988217725,-0.507308837623868)) ;
#48131=CARTESIAN_POINT('Ctrl Pts',(0.997265697009338,0.66977164251845,-0.639652621257518)) ;
#48132=CARTESIAN_POINT('Ctrl Pts',(0.800290746129714,0.690204620729973,
-0.874809910275015)) ;
#48133=CARTESIAN_POINT('Ctrl Pts',(0.676631046005103,0.701301073419951,
-0.973609034356905)) ;
#48134=CARTESIAN_POINT('Ctrl Pts',(0.403177716849776,0.723076512512997,
-1.11416703121241)) ;
#48135=CARTESIAN_POINT('Ctrl Pts',(0.257042102550089,0.733556992879919,
-1.15666275548468)) ;
#48136=CARTESIAN_POINT('Ctrl Pts',(-0.0465990627160015,0.753185598951027,
-1.18438080504815)) ;
#48137=CARTESIAN_POINT('Ctrl Pts',(-0.201291410338131,0.762614474487315,
-1.16808644012264)) ;
#48138=CARTESIAN_POINT('Ctrl Pts',(-0.496304589811692,0.783978003088777,
-1.07648945257075)) ;
#48139=CARTESIAN_POINT('Ctrl Pts',(-0.633609369050849,0.795056149017342,
-1.00184065511535)) ;
#48140=CARTESIAN_POINT('Ctrl Pts',(-0.867086037178609,0.816293390128693,
-0.807221339464417)) ;
#48141=CARTESIAN_POINT('Ctrl Pts',(-0.962388287817152,0.82601667662179,
-0.690806209974619)) ;
#48142=CARTESIAN_POINT('Ctrl Pts',(-1.1076412594506,0.845030925675896,-0.42265042921707)) ;
#48143=CARTESIAN_POINT('Ctrl Pts',(-1.15386377952163,0.855701220641653,
-0.272168479111453)) ;
#48144=CARTESIAN_POINT('Ctrl Pts',(-1.18463152093458,0.877487754511793,
0.0350845174872771)) ;
#48145=CARTESIAN_POINT('Ctrl Pts',(-1.17001865458337,0.888387649497562,
0.188804490427957)) ;
#48146=CARTESIAN_POINT('Ctrl Pts',(-1.08368335874431,0.908945399855658,
0.478728093627223)) ;
#48147=CARTESIAN_POINT('Ctrl Pts',(-1.01407322451917,0.917778187139484,
0.612537166206886)) ;
#48148=CARTESIAN_POINT('Ctrl Pts',(-0.82364121359487,0.937995371190235,
0.852940518897035)) ;
#48149=CARTESIAN_POINT('Ctrl Pts',(-0.702338222167855,0.949073319536787,
0.955299652901863)) ;
#48150=CARTESIAN_POINT('Ctrl Pts',(-0.431965145235364,0.970926219230269,
1.1033776390932)) ;
#48151=CARTESIAN_POINT('Ctrl Pts',(-0.286601196028543,0.981496568904902,
1.14974475965885)) ;
#48152=CARTESIAN_POINT('Ctrl Pts',(-0.0910484835269777,0.994315250465939,
1.1725983273716)) ;
#48153=CARTESIAN_POINT('Ctrl Pts',(-0.0455011814096055,0.997205878294077,
1.17524047358081)) ;
#48154=CARTESIAN_POINT('Ctrl Pts',(-4.39631847705415E-13,0.999999999999973,
1.17524047358083)) ;
#48155=CARTESIAN_POINT('Origin',(0.,-1.5,0.)) ;
#48156=CARTESIAN_POINT('',(1.375,-1.5,2.38156986040721)) ;
#48157=CARTESIAN_POINT('',(-1.375,-1.5,2.38156986040721)) ;
#48158=CARTESIAN_POINT('Origin',(0.,-1.5,0.)) ;
#48159=CARTESIAN_POINT('',(-1.62356638414832E-15,-1.25437990693814,3.17542648054294)) ;
#48160=CARTESIAN_POINT('Ctrl Pts',(-5.29571615987166E-11,-1.25437990692049,
3.17542648057351)) ;
#48161=CARTESIAN_POINT('Ctrl Pts',(0.736860279164301,-1.5,2.75000000001228)) ;
#48162=CARTESIAN_POINT('Ctrl Pts',(1.375,-1.5,2.3815698604072)) ;
#48163=CARTESIAN_POINT('Ctrl Pts',(-1.375,-1.5,2.3815698604072)) ;
#48164=CARTESIAN_POINT('Ctrl Pts',(-0.736860279164307,-1.5,2.75000000001228)) ;
#48165=CARTESIAN_POINT('Ctrl Pts',(5.29522918189065E-11,-1.25437990692049,
3.17542648057351)) ;
#48166=CARTESIAN_POINT('Origin',(0.,1.5,0.)) ;
#48167=CARTESIAN_POINT('',(-1.375,1.5,2.3815698604072)) ;
#48168=CARTESIAN_POINT('',(1.375,1.5,2.3815698604072)) ;
#48169=CARTESIAN_POINT('Origin',(0.,1.5,0.)) ;
#48170=CARTESIAN_POINT('',(-1.62356638414832E-15,1.25437990693814,3.17542648054294)) ;
#48171=CARTESIAN_POINT('Ctrl Pts',(-1.375,1.5,2.38156986040721)) ;
#48172=CARTESIAN_POINT('Ctrl Pts',(-0.736860279164303,1.5,2.75000000001229)) ;
#48173=CARTESIAN_POINT('Ctrl Pts',(5.29529270075774E-11,1.25437990692049,
3.17542648057351)) ;
#48174=CARTESIAN_POINT('Ctrl Pts',(-5.29455164730837E-11,1.25437990692049,
3.17542648057351)) ;
#48175=CARTESIAN_POINT('Ctrl Pts',(0.736860279164306,1.5,2.75000000001228)) ;
#48176=CARTESIAN_POINT('Ctrl Pts',(1.375,1.5,2.3815698604072)) ;
#48177=CARTESIAN_POINT('Ctrl Pts',(-0.00478010547540694,1.68781364799072,
-1.17519533396634)) ;
#48178=CARTESIAN_POINT('Ctrl Pts',(0.676909706932224,1.64604970885937,-1.17796810638181)) ;
#48179=CARTESIAN_POINT('Ctrl Pts',(1.01775743268642,1.60418711532683,-0.587602527731244)) ;
#48180=CARTESIAN_POINT('Ctrl Pts',(1.35700991024855,1.56252044866016,-8.30928921498564E-17)) ;
#48181=CARTESIAN_POINT('Ctrl Pts',(1.01775743268642,1.52085378199349,0.587602527731244)) ;
#48182=CARTESIAN_POINT('Ctrl Pts',(0.678504955124277,1.47918711532683,1.17520505546249)) ;
#48183=CARTESIAN_POINT('Ctrl Pts',(1.43921110951392E-16,1.43752044866016,
1.17520505546249)) ;
#48184=CARTESIAN_POINT('Ctrl Pts',(-0.678504955124276,1.39585378199349,
1.17520505546249)) ;
#48185=CARTESIAN_POINT('Ctrl Pts',(-1.01775743268641,1.35418711532683,0.587602527731245)) ;
#48186=CARTESIAN_POINT('Ctrl Pts',(-1.35700991024855,1.31252044866016,2.49278676449569E-16)) ;
#48187=CARTESIAN_POINT('Ctrl Pts',(-1.01775743268642,1.27085378199349,-0.587602527731243)) ;
#48188=CARTESIAN_POINT('Ctrl Pts',(-0.678504955124277,1.22918711532683,
-1.17520505546249)) ;
#48189=CARTESIAN_POINT('Ctrl Pts',(0.,1.18752044866016,-1.17520505546249)) ;
#48190=CARTESIAN_POINT('Ctrl Pts',(0.678504955124277,1.14585378199349,-1.17520505546249)) ;
#48191=CARTESIAN_POINT('Ctrl Pts',(1.01775743268642,1.10418711532683,-0.587602527731244)) ;
#48192=CARTESIAN_POINT('Ctrl Pts',(1.35700991024855,1.06252044866016,-8.30928921498564E-17)) ;
#48193=CARTESIAN_POINT('Ctrl Pts',(1.01775743268642,1.02085378199349,0.587602527731244)) ;
#48194=CARTESIAN_POINT('Ctrl Pts',(0.678504955124277,0.979187115326827,
1.17520505546249)) ;
#48195=CARTESIAN_POINT('Ctrl Pts',(1.43921110951392E-16,0.937520448660161,
1.17520505546249)) ;
#48196=CARTESIAN_POINT('Ctrl Pts',(-0.678504955124276,0.895853781993494,
1.17520505546249)) ;
#48197=CARTESIAN_POINT('Ctrl Pts',(-1.01775743268641,0.854187115326828,
0.587602527731245)) ;
#48198=CARTESIAN_POINT('Ctrl Pts',(-1.35700991024855,0.812520448660161,
2.49278676449569E-16)) ;
#48199=CARTESIAN_POINT('Ctrl Pts',(-1.01775743268642,0.770853781993494,
-0.587602527731243)) ;
#48200=CARTESIAN_POINT('Ctrl Pts',(-0.678504955124277,0.729187115326828,
-1.17520505546249)) ;
#48201=CARTESIAN_POINT('Ctrl Pts',(0.,0.687520448660161,-1.17520505546249)) ;
#48202=CARTESIAN_POINT('Ctrl Pts',(0.678504955124277,0.645853781993494,
-1.17520505546249)) ;
#48203=CARTESIAN_POINT('Ctrl Pts',(1.01775743268642,0.604187115326828,-0.587602527731244)) ;
#48204=CARTESIAN_POINT('Ctrl Pts',(1.35700991024855,0.562520448660161,-8.30928921498564E-17)) ;
#48205=CARTESIAN_POINT('Ctrl Pts',(1.01775743268642,0.520853781993494,0.587602527731244)) ;
#48206=CARTESIAN_POINT('Ctrl Pts',(0.678504955124277,0.479187115326828,
1.17520505546249)) ;
#48207=CARTESIAN_POINT('Ctrl Pts',(1.43921110951392E-16,0.437520448660161,
1.17520505546249)) ;
#48208=CARTESIAN_POINT('Ctrl Pts',(-0.678504955124276,0.395853781993494,
1.17520505546249)) ;
#48209=CARTESIAN_POINT('Ctrl Pts',(-1.01775743268641,0.354187115326828,
0.587602527731245)) ;
#48210=CARTESIAN_POINT('Ctrl Pts',(-1.35700991024855,0.312520448660161,
2.49278676449569E-16)) ;
#48211=CARTESIAN_POINT('Ctrl Pts',(-1.01775743268642,0.270853781993494,
-0.587602527731243)) ;
#48212=CARTESIAN_POINT('Ctrl Pts',(-0.678504955124277,0.229187115326828,
-1.17520505546249)) ;
#48213=CARTESIAN_POINT('Ctrl Pts',(0.,0.187520448660161,-1.17520505546249)) ;
#48214=CARTESIAN_POINT('Ctrl Pts',(0.678504955124277,0.145853781993494,
-1.17520505546249)) ;
#48215=CARTESIAN_POINT('Ctrl Pts',(1.01775743268642,0.104187115326828,-0.587602527731244)) ;
#48216=CARTESIAN_POINT('Ctrl Pts',(1.35700991024855,0.0625204486601609,
-8.30928921498564E-17)) ;
#48217=CARTESIAN_POINT('Ctrl Pts',(1.01775743268642,0.0208537819934942,
0.587602527731244)) ;
#48218=CARTESIAN_POINT('Ctrl Pts',(0.678504955124277,-0.0208128846731724,
1.17520505546249)) ;
#48219=CARTESIAN_POINT('Ctrl Pts',(1.43921110951392E-16,-0.0624795513398393,
1.17520505546249)) ;
#48220=CARTESIAN_POINT('Ctrl Pts',(-0.678504955124276,-0.104146218006506,
1.17520505546249)) ;
#48221=CARTESIAN_POINT('Ctrl Pts',(-1.01775743268641,-0.145812884673173,
0.587602527731245)) ;
#48222=CARTESIAN_POINT('Ctrl Pts',(-1.35700991024855,-0.187479551339839,
2.49278676449569E-16)) ;
#48223=CARTESIAN_POINT('Ctrl Pts',(-1.01775743268642,-0.229146218006506,
-0.587602527731243)) ;
#48224=CARTESIAN_POINT('Ctrl Pts',(-0.678504955124277,-0.270812884673172,
-1.17520505546249)) ;
#48225=CARTESIAN_POINT('Ctrl Pts',(0.,-0.312479551339839,-1.17520505546249)) ;
#48226=CARTESIAN_POINT('Ctrl Pts',(0.678504955124277,-0.354146218006506,
-1.17520505546249)) ;
#48227=CARTESIAN_POINT('Ctrl Pts',(1.01775743268642,-0.395812884673173,
-0.587602527731244)) ;
#48228=CARTESIAN_POINT('Ctrl Pts',(1.35700991024855,-0.437479551339839,
-8.30928921498564E-17)) ;
#48229=CARTESIAN_POINT('Ctrl Pts',(1.01775743268642,-0.479146218006506,
0.587602527731244)) ;
#48230=CARTESIAN_POINT('Ctrl Pts',(0.678504955124277,-0.520812884673173,
1.17520505546249)) ;
#48231=CARTESIAN_POINT('Ctrl Pts',(1.43921110951392E-16,-0.562479551339839,
1.17520505546249)) ;
#48232=CARTESIAN_POINT('Ctrl Pts',(-0.678504955124276,-0.604146218006506,
1.17520505546249)) ;
#48233=CARTESIAN_POINT('Ctrl Pts',(-1.01775743268641,-0.645812884673172,
0.587602527731245)) ;
#48234=CARTESIAN_POINT('Ctrl Pts',(-1.35700991024855,-0.687479551339839,
2.49278676449569E-16)) ;
#48235=CARTESIAN_POINT('Ctrl Pts',(-1.01775743268642,-0.729146218006506,
-0.587602527731243)) ;
#48236=CARTESIAN_POINT('Ctrl Pts',(-0.678504955124277,-0.770812884673173,
-1.17520505546249)) ;
#48237=CARTESIAN_POINT('Ctrl Pts',(0.,-0.812479551339839,-1.17520505546249)) ;
#48238=CARTESIAN_POINT('Ctrl Pts',(0.678504955124277,-0.854146218006506,
-1.17520505546249)) ;
#48239=CARTESIAN_POINT('Ctrl Pts',(1.01775743268642,-0.895812884673173,
-0.587602527731244)) ;
#48240=CARTESIAN_POINT('Ctrl Pts',(1.35700991024855,-0.937479551339839,
-8.30928921498564E-17)) ;
#48241=CARTESIAN_POINT('Ctrl Pts',(1.01775743268642,-0.979146218006506,
0.587602527731244)) ;
#48242=CARTESIAN_POINT('Ctrl Pts',(0.678504955124277,-1.02081288467317,
1.17520505546249)) ;
#48243=CARTESIAN_POINT('Ctrl Pts',(1.43921110951392E-16,-1.06247955133984,
1.17520505546249)) ;
#48244=CARTESIAN_POINT('Ctrl Pts',(-0.678504955124276,-1.10414621800651,
1.17520505546249)) ;
#48245=CARTESIAN_POINT('Ctrl Pts',(-1.01775743268641,-1.14581288467317,
0.587602527731245)) ;
#48246=CARTESIAN_POINT('Ctrl Pts',(-1.35700991024855,-1.18747955133984,
2.49278676449569E-16)) ;
#48247=CARTESIAN_POINT('Ctrl Pts',(-1.01775743268642,-1.22914621800651,
-0.587602527731243)) ;
#48248=CARTESIAN_POINT('Ctrl Pts',(-0.678504955124277,-1.27081288467317,
-1.17520505546249)) ;
#48249=CARTESIAN_POINT('Ctrl Pts',(0.,-1.31247955133984,-1.17520505546249)) ;
#48250=CARTESIAN_POINT('Ctrl Pts',(0.678504955124277,-1.35414621800651,
-1.17520505546249)) ;
#48251=CARTESIAN_POINT('Ctrl Pts',(1.01775743268642,-1.39581288467317,-0.587602527731244)) ;
#48252=CARTESIAN_POINT('Ctrl Pts',(1.35700991024855,-1.43747955133984,-8.30928921498564E-17)) ;
#48253=CARTESIAN_POINT('Ctrl Pts',(1.01775743268642,-1.47914621800651,0.587602527731244)) ;
#48254=CARTESIAN_POINT('Ctrl Pts',(0.678504955124277,-1.52081288467317,
1.17520505546249)) ;
#48255=CARTESIAN_POINT('Ctrl Pts',(1.43921110951392E-16,-1.56247955133984,
1.17520505546249)) ;
#48256=CARTESIAN_POINT('Ctrl Pts',(-0.678504955124276,-1.60414621800651,
1.17520505546249)) ;
#48257=CARTESIAN_POINT('Ctrl Pts',(-1.01775743268641,-1.64581288467317,
0.587602527731245)) ;
#48258=CARTESIAN_POINT('Ctrl Pts',(-1.35700991024855,-1.68747955133984,
2.49278676449569E-16)) ;
#48259=CARTESIAN_POINT('Ctrl Pts',(-1.01775743268642,-1.72914621800651,
-0.587602527731243)) ;
#48260=CARTESIAN_POINT('Ctrl Pts',(-0.678504955124277,-1.77081288467317,
-1.17520505546249)) ;
#48261=CARTESIAN_POINT('Ctrl Pts',(0.,-1.81247955133984,-1.17520505546249)) ;
#48262=CARTESIAN_POINT('Ctrl Pts',(-0.00610134161874418,1.5002727506704,
-1.50002300957017)) ;
#48263=CARTESIAN_POINT('Ctrl Pts',(0.864009672649723,1.45850881153905,-1.50356218497642)) ;
#48264=CARTESIAN_POINT('Ctrl Pts',(1.2990687786669,1.41664621800651,-0.750017709059173)) ;
#48265=CARTESIAN_POINT('Ctrl Pts',(1.7320917048892,1.37497955133984,-1.06060028111112E-16)) ;
#48266=CARTESIAN_POINT('Ctrl Pts',(1.2990687786669,1.33331288467317,0.750017709059172)) ;
#48267=CARTESIAN_POINT('Ctrl Pts',(0.8660458524446,1.29164621800651,1.50003541811835)) ;
#48268=CARTESIAN_POINT('Ctrl Pts',(1.83701357340629E-16,1.24997955133984,
1.50003541811835)) ;
#48269=CARTESIAN_POINT('Ctrl Pts',(-0.866045852444599,1.20831288467317,
1.50003541811835)) ;
#48270=CARTESIAN_POINT('Ctrl Pts',(-1.2990687786669,1.16664621800651,0.750017709059173)) ;
#48271=CARTESIAN_POINT('Ctrl Pts',(-1.7320917048892,1.12497955133984,3.18180084333336E-16)) ;
#48272=CARTESIAN_POINT('Ctrl Pts',(-1.2990687786669,1.08331288467317,-0.750017709059171)) ;
#48273=CARTESIAN_POINT('Ctrl Pts',(-0.8660458524446,1.04164621800651,-1.50003541811835)) ;
#48274=CARTESIAN_POINT('Ctrl Pts',(0.,0.99997955133984,-1.50003541811835)) ;
#48275=CARTESIAN_POINT('Ctrl Pts',(0.866045852444599,0.958312884673173,
-1.50003541811835)) ;
#48276=CARTESIAN_POINT('Ctrl Pts',(1.2990687786669,0.916646218006506,-0.750017709059173)) ;
#48277=CARTESIAN_POINT('Ctrl Pts',(1.7320917048892,0.87497955133984,-1.06060028111112E-16)) ;
#48278=CARTESIAN_POINT('Ctrl Pts',(1.2990687786669,0.833312884673173,0.750017709059172)) ;
#48279=CARTESIAN_POINT('Ctrl Pts',(0.8660458524446,0.791646218006506,1.50003541811835)) ;
#48280=CARTESIAN_POINT('Ctrl Pts',(1.83701357340629E-16,0.749979551339839,
1.50003541811835)) ;
#48281=CARTESIAN_POINT('Ctrl Pts',(-0.866045852444599,0.708312884673173,
1.50003541811835)) ;
#48282=CARTESIAN_POINT('Ctrl Pts',(-1.2990687786669,0.666646218006506,0.750017709059173)) ;
#48283=CARTESIAN_POINT('Ctrl Pts',(-1.7320917048892,0.624979551339839,3.18180084333336E-16)) ;
#48284=CARTESIAN_POINT('Ctrl Pts',(-1.2990687786669,0.583312884673173,-0.750017709059171)) ;
#48285=CARTESIAN_POINT('Ctrl Pts',(-0.8660458524446,0.541646218006506,-1.50003541811835)) ;
#48286=CARTESIAN_POINT('Ctrl Pts',(0.,0.499979551339839,-1.50003541811835)) ;
#48287=CARTESIAN_POINT('Ctrl Pts',(0.866045852444599,0.458312884673173,
-1.50003541811835)) ;
#48288=CARTESIAN_POINT('Ctrl Pts',(1.2990687786669,0.416646218006506,-0.750017709059173)) ;
#48289=CARTESIAN_POINT('Ctrl Pts',(1.7320917048892,0.37497955133984,-1.06060028111112E-16)) ;
#48290=CARTESIAN_POINT('Ctrl Pts',(1.2990687786669,0.333312884673173,0.750017709059172)) ;
#48291=CARTESIAN_POINT('Ctrl Pts',(0.8660458524446,0.291646218006506,1.50003541811835)) ;
#48292=CARTESIAN_POINT('Ctrl Pts',(1.83701357340629E-16,0.249979551339839,
1.50003541811835)) ;
#48293=CARTESIAN_POINT('Ctrl Pts',(-0.866045852444599,0.208312884673173,
1.50003541811835)) ;
#48294=CARTESIAN_POINT('Ctrl Pts',(-1.2990687786669,0.166646218006506,0.750017709059173)) ;
#48295=CARTESIAN_POINT('Ctrl Pts',(-1.7320917048892,0.12497955133984,3.18180084333336E-16)) ;
#48296=CARTESIAN_POINT('Ctrl Pts',(-1.2990687786669,0.0833128846731729,
-0.750017709059171)) ;
#48297=CARTESIAN_POINT('Ctrl Pts',(-0.8660458524446,0.0416462180065062,
-1.50003541811835)) ;
#48298=CARTESIAN_POINT('Ctrl Pts',(0.,-2.0448660160613E-5,-1.50003541811835)) ;
#48299=CARTESIAN_POINT('Ctrl Pts',(0.866045852444599,-0.0416871153268273,
-1.50003541811835)) ;
#48300=CARTESIAN_POINT('Ctrl Pts',(1.2990687786669,-0.0833537819934939,
-0.750017709059173)) ;
#48301=CARTESIAN_POINT('Ctrl Pts',(1.7320917048892,-0.125020448660161,-1.06060028111112E-16)) ;
#48302=CARTESIAN_POINT('Ctrl Pts',(1.2990687786669,-0.166687115326827,0.750017709059172)) ;
#48303=CARTESIAN_POINT('Ctrl Pts',(0.8660458524446,-0.208353781993494,1.50003541811835)) ;
#48304=CARTESIAN_POINT('Ctrl Pts',(1.83701357340629E-16,-0.250020448660161,
1.50003541811835)) ;
#48305=CARTESIAN_POINT('Ctrl Pts',(-0.866045852444599,-0.291687115326827,
1.50003541811835)) ;
#48306=CARTESIAN_POINT('Ctrl Pts',(-1.2990687786669,-0.333353781993494,
0.750017709059173)) ;
#48307=CARTESIAN_POINT('Ctrl Pts',(-1.7320917048892,-0.375020448660161,
3.18180084333336E-16)) ;
#48308=CARTESIAN_POINT('Ctrl Pts',(-1.2990687786669,-0.416687115326827,
-0.750017709059171)) ;
#48309=CARTESIAN_POINT('Ctrl Pts',(-0.8660458524446,-0.458353781993494,
-1.50003541811835)) ;
#48310=CARTESIAN_POINT('Ctrl Pts',(0.,-0.500020448660161,-1.50003541811835)) ;
#48311=CARTESIAN_POINT('Ctrl Pts',(0.866045852444599,-0.541687115326827,
-1.50003541811835)) ;
#48312=CARTESIAN_POINT('Ctrl Pts',(1.2990687786669,-0.583353781993494,-0.750017709059173)) ;
#48313=CARTESIAN_POINT('Ctrl Pts',(1.7320917048892,-0.62502044866016,-1.06060028111112E-16)) ;
#48314=CARTESIAN_POINT('Ctrl Pts',(1.2990687786669,-0.666687115326827,0.750017709059172)) ;
#48315=CARTESIAN_POINT('Ctrl Pts',(0.8660458524446,-0.708353781993494,1.50003541811835)) ;
#48316=CARTESIAN_POINT('Ctrl Pts',(1.83701357340629E-16,-0.75002044866016,
1.50003541811835)) ;
#48317=CARTESIAN_POINT('Ctrl Pts',(-0.866045852444599,-0.791687115326827,
1.50003541811835)) ;
#48318=CARTESIAN_POINT('Ctrl Pts',(-1.2990687786669,-0.833353781993494,
0.750017709059173)) ;
#48319=CARTESIAN_POINT('Ctrl Pts',(-1.7320917048892,-0.87502044866016,3.18180084333336E-16)) ;
#48320=CARTESIAN_POINT('Ctrl Pts',(-1.2990687786669,-0.916687115326827,
-0.750017709059171)) ;
#48321=CARTESIAN_POINT('Ctrl Pts',(-0.8660458524446,-0.958353781993494,
-1.50003541811835)) ;
#48322=CARTESIAN_POINT('Ctrl Pts',(0.,-1.00002044866016,-1.50003541811835)) ;
#48323=CARTESIAN_POINT('Ctrl Pts',(0.866045852444599,-1.04168711532683,
-1.50003541811835)) ;
#48324=CARTESIAN_POINT('Ctrl Pts',(1.2990687786669,-1.08335378199349,-0.750017709059173)) ;
#48325=CARTESIAN_POINT('Ctrl Pts',(1.7320917048892,-1.12502044866016,-1.06060028111112E-16)) ;
#48326=CARTESIAN_POINT('Ctrl Pts',(1.2990687786669,-1.16668711532683,0.750017709059172)) ;
#48327=CARTESIAN_POINT('Ctrl Pts',(0.8660458524446,-1.20835378199349,1.50003541811835)) ;
#48328=CARTESIAN_POINT('Ctrl Pts',(1.83701357340629E-16,-1.25002044866016,
1.50003541811835)) ;
#48329=CARTESIAN_POINT('Ctrl Pts',(-0.866045852444599,-1.29168711532683,
1.50003541811835)) ;
#48330=CARTESIAN_POINT('Ctrl Pts',(-1.2990687786669,-1.33335378199349,0.750017709059173)) ;
#48331=CARTESIAN_POINT('Ctrl Pts',(-1.7320917048892,-1.37502044866016,3.18180084333336E-16)) ;
#48332=CARTESIAN_POINT('Ctrl Pts',(-1.2990687786669,-1.41668711532683,-0.750017709059171)) ;
#48333=CARTESIAN_POINT('Ctrl Pts',(-0.8660458524446,-1.45835378199349,-1.50003541811835)) ;
#48334=CARTESIAN_POINT('Ctrl Pts',(0.,-1.50002044866016,-1.50003541811835)) ;
#48335=CARTESIAN_POINT('Ctrl Pts',(0.866045852444599,-1.54168711532683,
-1.50003541811835)) ;
#48336=CARTESIAN_POINT('Ctrl Pts',(1.2990687786669,-1.58335378199349,-0.750017709059173)) ;
#48337=CARTESIAN_POINT('Ctrl Pts',(1.7320917048892,-1.62502044866016,-1.06060028111112E-16)) ;
#48338=CARTESIAN_POINT('Ctrl Pts',(1.2990687786669,-1.66668711532683,0.750017709059172)) ;
#48339=CARTESIAN_POINT('Ctrl Pts',(0.8660458524446,-1.70835378199349,1.50003541811835)) ;
#48340=CARTESIAN_POINT('Ctrl Pts',(1.83701357340629E-16,-1.75002044866016,
1.50003541811835)) ;
#48341=CARTESIAN_POINT('Ctrl Pts',(-0.866045852444599,-1.79168711532683,
1.50003541811835)) ;
#48342=CARTESIAN_POINT('Ctrl Pts',(-1.2990687786669,-1.83335378199349,0.750017709059173)) ;
#48343=CARTESIAN_POINT('Ctrl Pts',(-1.7320917048892,-1.87502044866016,3.18180084333336E-16)) ;
#48344=CARTESIAN_POINT('Ctrl Pts',(-1.2990687786669,-1.91668711532683,-0.750017709059171)) ;
#48345=CARTESIAN_POINT('Ctrl Pts',(-0.8660458524446,-1.95835378199349,-1.50003541811835)) ;
#48346=CARTESIAN_POINT('Ctrl Pts',(0.,-2.00002044866016,-1.50003541811835)) ;
#48347=CARTESIAN_POINT('Ctrl Pts',(0.,1.93751828185976,-1.50003166510997)) ;
#48348=CARTESIAN_POINT('Ctrl Pts',(0.866043685644202,1.89585161519309,-1.50003166510997)) ;
#48349=CARTESIAN_POINT('Ctrl Pts',(1.2990655284663,1.85418494852643,-0.750015832554983)) ;
#48350=CARTESIAN_POINT('Ctrl Pts',(1.73208737128841,1.81251828185976,-1.06059762754595E-16)) ;
#48351=CARTESIAN_POINT('Ctrl Pts',(1.2990655284663,1.77085161519309,0.750015832554983)) ;
#48352=CARTESIAN_POINT('Ctrl Pts',(0.866043685644202,1.72918494852643,1.50003166510997)) ;
#48353=CARTESIAN_POINT('Ctrl Pts',(1.83700897729659E-16,1.68751828185976,
1.50003166510997)) ;
#48354=CARTESIAN_POINT('Ctrl Pts',(-0.866043685644201,1.64585161519309,
1.50003166510997)) ;
#48355=CARTESIAN_POINT('Ctrl Pts',(-1.2990655284663,1.60418494852643,0.750015832554984)) ;
#48356=CARTESIAN_POINT('Ctrl Pts',(-1.73208737128841,1.56251828185976,3.18179288263784E-16)) ;
#48357=CARTESIAN_POINT('Ctrl Pts',(-1.2990655284663,1.52085161519309,-0.750015832554982)) ;
#48358=CARTESIAN_POINT('Ctrl Pts',(-0.866043685644203,1.47918494852643,
-1.50003166510997)) ;
#48359=CARTESIAN_POINT('Ctrl Pts',(0.,1.43751828185976,-1.50003166510997)) ;
#48360=CARTESIAN_POINT('Ctrl Pts',(0.866043685644202,1.39585161519309,-1.50003166510997)) ;
#48361=CARTESIAN_POINT('Ctrl Pts',(1.2990655284663,1.35418494852643,-0.750015832554983)) ;
#48362=CARTESIAN_POINT('Ctrl Pts',(1.73208737128841,1.31251828185976,-1.06059762754595E-16)) ;
#48363=CARTESIAN_POINT('Ctrl Pts',(1.2990655284663,1.27085161519309,0.750015832554983)) ;
#48364=CARTESIAN_POINT('Ctrl Pts',(0.866043685644202,1.22918494852643,1.50003166510997)) ;
#48365=CARTESIAN_POINT('Ctrl Pts',(1.83700897729659E-16,1.18751828185976,
1.50003166510997)) ;
#48366=CARTESIAN_POINT('Ctrl Pts',(-0.866043685644201,1.14585161519309,
1.50003166510997)) ;
#48367=CARTESIAN_POINT('Ctrl Pts',(-1.2990655284663,1.10418494852643,0.750015832554984)) ;
#48368=CARTESIAN_POINT('Ctrl Pts',(-1.73208737128841,1.06251828185976,3.18179288263784E-16)) ;
#48369=CARTESIAN_POINT('Ctrl Pts',(-1.2990655284663,1.02085161519309,-0.750015832554982)) ;
#48370=CARTESIAN_POINT('Ctrl Pts',(-0.866043685644203,0.97918494852643,
-1.50003166510997)) ;
#48371=CARTESIAN_POINT('Ctrl Pts',(0.,0.937518281859764,-1.50003166510997)) ;
#48372=CARTESIAN_POINT('Ctrl Pts',(0.866043685644202,0.895851615193097,
-1.50003166510997)) ;
#48373=CARTESIAN_POINT('Ctrl Pts',(1.2990655284663,0.85418494852643,-0.750015832554983)) ;
#48374=CARTESIAN_POINT('Ctrl Pts',(1.73208737128841,0.812518281859764,-1.06059762754595E-16)) ;
#48375=CARTESIAN_POINT('Ctrl Pts',(1.2990655284663,0.770851615193097,0.750015832554983)) ;
#48376=CARTESIAN_POINT('Ctrl Pts',(0.866043685644202,0.72918494852643,1.50003166510997)) ;
#48377=CARTESIAN_POINT('Ctrl Pts',(1.83700897729659E-16,0.687518281859763,
1.50003166510997)) ;
#48378=CARTESIAN_POINT('Ctrl Pts',(-0.866043685644201,0.645851615193097,
1.50003166510997)) ;
#48379=CARTESIAN_POINT('Ctrl Pts',(-1.2990655284663,0.60418494852643,0.750015832554984)) ;
#48380=CARTESIAN_POINT('Ctrl Pts',(-1.73208737128841,0.562518281859763,
3.18179288263784E-16)) ;
#48381=CARTESIAN_POINT('Ctrl Pts',(-1.2990655284663,0.520851615193097,-0.750015832554982)) ;
#48382=CARTESIAN_POINT('Ctrl Pts',(-0.866043685644203,0.47918494852643,
-1.50003166510997)) ;
#48383=CARTESIAN_POINT('Ctrl Pts',(0.,0.437518281859763,-1.50003166510997)) ;
#48384=CARTESIAN_POINT('Ctrl Pts',(0.866043685644202,0.395851615193097,
-1.50003166510997)) ;
#48385=CARTESIAN_POINT('Ctrl Pts',(1.2990655284663,0.35418494852643,-0.750015832554983)) ;
#48386=CARTESIAN_POINT('Ctrl Pts',(1.73208737128841,0.312518281859763,-1.06059762754595E-16)) ;
#48387=CARTESIAN_POINT('Ctrl Pts',(1.2990655284663,0.270851615193097,0.750015832554983)) ;
#48388=CARTESIAN_POINT('Ctrl Pts',(0.866043685644202,0.22918494852643,1.50003166510997)) ;
#48389=CARTESIAN_POINT('Ctrl Pts',(1.83700897729659E-16,0.187518281859763,
1.50003166510997)) ;
#48390=CARTESIAN_POINT('Ctrl Pts',(-0.866043685644201,0.145851615193097,
1.50003166510997)) ;
#48391=CARTESIAN_POINT('Ctrl Pts',(-1.2990655284663,0.10418494852643,0.750015832554984)) ;
#48392=CARTESIAN_POINT('Ctrl Pts',(-1.73208737128841,0.0625182818597633,
3.18179288263784E-16)) ;
#48393=CARTESIAN_POINT('Ctrl Pts',(-1.2990655284663,0.0208516151930967,
-0.750015832554982)) ;
#48394=CARTESIAN_POINT('Ctrl Pts',(-0.866043685644203,-0.02081505147357,
-1.50003166510997)) ;
#48395=CARTESIAN_POINT('Ctrl Pts',(0.,-0.0624817181402368,-1.50003166510997)) ;
#48396=CARTESIAN_POINT('Ctrl Pts',(0.866043685644202,-0.104148384806903,
-1.50003166510997)) ;
#48397=CARTESIAN_POINT('Ctrl Pts',(1.2990655284663,-0.14581505147357,-0.750015832554983)) ;
#48398=CARTESIAN_POINT('Ctrl Pts',(1.73208737128841,-0.187481718140236,
-1.06059762754595E-16)) ;
#48399=CARTESIAN_POINT('Ctrl Pts',(1.2990655284663,-0.229148384806903,0.750015832554983)) ;
#48400=CARTESIAN_POINT('Ctrl Pts',(0.866043685644202,-0.27081505147357,
1.50003166510997)) ;
#48401=CARTESIAN_POINT('Ctrl Pts',(1.83700897729659E-16,-0.312481718140236,
1.50003166510997)) ;
#48402=CARTESIAN_POINT('Ctrl Pts',(-0.866043685644201,-0.354148384806903,
1.50003166510997)) ;
#48403=CARTESIAN_POINT('Ctrl Pts',(-1.2990655284663,-0.39581505147357,0.750015832554984)) ;
#48404=CARTESIAN_POINT('Ctrl Pts',(-1.73208737128841,-0.437481718140237,
3.18179288263784E-16)) ;
#48405=CARTESIAN_POINT('Ctrl Pts',(-1.2990655284663,-0.479148384806903,
-0.750015832554982)) ;
#48406=CARTESIAN_POINT('Ctrl Pts',(-0.866043685644203,-0.52081505147357,
-1.50003166510997)) ;
#48407=CARTESIAN_POINT('Ctrl Pts',(0.,-0.562481718140237,-1.50003166510997)) ;
#48408=CARTESIAN_POINT('Ctrl Pts',(0.866043685644202,-0.604148384806903,
-1.50003166510997)) ;
#48409=CARTESIAN_POINT('Ctrl Pts',(1.2990655284663,-0.64581505147357,-0.750015832554983)) ;
#48410=CARTESIAN_POINT('Ctrl Pts',(1.73208737128841,-0.687481718140236,
-1.06059762754595E-16)) ;
#48411=CARTESIAN_POINT('Ctrl Pts',(1.2990655284663,-0.729148384806903,0.750015832554983)) ;
#48412=CARTESIAN_POINT('Ctrl Pts',(0.866043685644202,-0.77081505147357,
1.50003166510997)) ;
#48413=CARTESIAN_POINT('Ctrl Pts',(1.83700897729659E-16,-0.812481718140236,
1.50003166510997)) ;
#48414=CARTESIAN_POINT('Ctrl Pts',(-0.866043685644201,-0.854148384806903,
1.50003166510997)) ;
#48415=CARTESIAN_POINT('Ctrl Pts',(-1.2990655284663,-0.89581505147357,0.750015832554984)) ;
#48416=CARTESIAN_POINT('Ctrl Pts',(-1.73208737128841,-0.937481718140237,
3.18179288263784E-16)) ;
#48417=CARTESIAN_POINT('Ctrl Pts',(-1.2990655284663,-0.979148384806903,
-0.750015832554982)) ;
#48418=CARTESIAN_POINT('Ctrl Pts',(-0.866043685644203,-1.02081505147357,
-1.50003166510997)) ;
#48419=CARTESIAN_POINT('Ctrl Pts',(0.,-1.06248171814024,-1.50003166510997)) ;
#48420=CARTESIAN_POINT('Ctrl Pts',(0.866043685644202,-1.10414838480691,
-1.50003166510997)) ;
#48421=CARTESIAN_POINT('Ctrl Pts',(1.2990655284663,-1.14581505147357,-0.750015832554983)) ;
#48422=CARTESIAN_POINT('Ctrl Pts',(1.73208737128841,-1.18748171814024,-1.06059762754595E-16)) ;
#48423=CARTESIAN_POINT('Ctrl Pts',(1.2990655284663,-1.22914838480691,0.750015832554983)) ;
#48424=CARTESIAN_POINT('Ctrl Pts',(0.866043685644202,-1.27081505147357,
1.50003166510997)) ;
#48425=CARTESIAN_POINT('Ctrl Pts',(1.83700897729659E-16,-1.31248171814024,
1.50003166510997)) ;
#48426=CARTESIAN_POINT('Ctrl Pts',(-0.866043685644201,-1.35414838480691,
1.50003166510997)) ;
#48427=CARTESIAN_POINT('Ctrl Pts',(-1.2990655284663,-1.39581505147357,0.750015832554984)) ;
#48428=CARTESIAN_POINT('Ctrl Pts',(-1.73208737128841,-1.43748171814024,
3.18179288263784E-16)) ;
#48429=CARTESIAN_POINT('Ctrl Pts',(-1.2990655284663,-1.47914838480691,-0.750015832554982)) ;
#48430=CARTESIAN_POINT('Ctrl Pts',(-0.866043685644203,-1.52081505147357,
-1.50003166510997)) ;
#48431=CARTESIAN_POINT('Ctrl Pts',(0.,-1.56248171814024,-1.50003166510997)) ;
#48432=CARTESIAN_POINT('Ctrl Pts',(0.,1.75,-1.17524047358083)) ;
#48433=CARTESIAN_POINT('Ctrl Pts',(0.678525403784437,1.70833333333333,-1.17524047358083)) ;
#48434=CARTESIAN_POINT('Ctrl Pts',(1.01778810567666,1.66666666666667,-0.587620236790417)) ;
#48435=CARTESIAN_POINT('Ctrl Pts',(1.35705080756887,1.625,-8.30953963884777E-17)) ;
#48436=CARTESIAN_POINT('Ctrl Pts',(1.01778810567666,1.58333333333333,0.587620236790416)) ;
#48437=CARTESIAN_POINT('Ctrl Pts',(0.678525403784438,1.54166666666667,1.17524047358083)) ;
#48438=CARTESIAN_POINT('Ctrl Pts',(1.43925448419919E-16,1.5,1.17524047358083)) ;
#48439=CARTESIAN_POINT('Ctrl Pts',(-0.678525403784437,1.45833333333333,
1.17524047358083)) ;
#48440=CARTESIAN_POINT('Ctrl Pts',(-1.01778810567666,1.41666666666667,0.587620236790417)) ;
#48441=CARTESIAN_POINT('Ctrl Pts',(-1.35705080756887,1.375,2.49286189165433E-16)) ;
#48442=CARTESIAN_POINT('Ctrl Pts',(-1.01778810567666,1.33333333333333,-0.587620236790416)) ;
#48443=CARTESIAN_POINT('Ctrl Pts',(-0.678525403784438,1.29166666666667,
-1.17524047358083)) ;
#48444=CARTESIAN_POINT('Ctrl Pts',(0.,1.25,-1.17524047358083)) ;
#48445=CARTESIAN_POINT('Ctrl Pts',(0.678525403784437,1.20833333333333,-1.17524047358083)) ;
#48446=CARTESIAN_POINT('Ctrl Pts',(1.01778810567666,1.16666666666667,-0.587620236790417)) ;
#48447=CARTESIAN_POINT('Ctrl Pts',(1.35705080756887,1.125,-8.30953963884777E-17)) ;
#48448=CARTESIAN_POINT('Ctrl Pts',(1.01778810567666,1.08333333333333,0.587620236790416)) ;
#48449=CARTESIAN_POINT('Ctrl Pts',(0.678525403784438,1.04166666666667,1.17524047358083)) ;
#48450=CARTESIAN_POINT('Ctrl Pts',(1.43925448419919E-16,1.,1.17524047358083)) ;
#48451=CARTESIAN_POINT('Ctrl Pts',(-0.678525403784437,0.958333333333334,
1.17524047358083)) ;
#48452=CARTESIAN_POINT('Ctrl Pts',(-1.01778810567666,0.916666666666667,
0.587620236790417)) ;
#48453=CARTESIAN_POINT('Ctrl Pts',(-1.35705080756887,0.875,2.49286189165433E-16)) ;
#48454=CARTESIAN_POINT('Ctrl Pts',(-1.01778810567666,0.833333333333334,
-0.587620236790416)) ;
#48455=CARTESIAN_POINT('Ctrl Pts',(-0.678525403784438,0.791666666666667,
-1.17524047358083)) ;
#48456=CARTESIAN_POINT('Ctrl Pts',(0.,0.75,-1.17524047358083)) ;
#48457=CARTESIAN_POINT('Ctrl Pts',(0.678525403784437,0.708333333333334,
-1.17524047358083)) ;
#48458=CARTESIAN_POINT('Ctrl Pts',(1.01778810567666,0.666666666666667,-0.587620236790417)) ;
#48459=CARTESIAN_POINT('Ctrl Pts',(1.35705080756887,0.625,-8.30953963884777E-17)) ;
#48460=CARTESIAN_POINT('Ctrl Pts',(1.01778810567666,0.583333333333334,0.587620236790416)) ;
#48461=CARTESIAN_POINT('Ctrl Pts',(0.678525403784438,0.541666666666667,
1.17524047358083)) ;
#48462=CARTESIAN_POINT('Ctrl Pts',(1.43925448419919E-16,0.5,1.17524047358083)) ;
#48463=CARTESIAN_POINT('Ctrl Pts',(-0.678525403784437,0.458333333333334,
1.17524047358083)) ;
#48464=CARTESIAN_POINT('Ctrl Pts',(-1.01778810567666,0.416666666666667,
0.587620236790417)) ;
#48465=CARTESIAN_POINT('Ctrl Pts',(-1.35705080756887,0.375,2.49286189165433E-16)) ;
#48466=CARTESIAN_POINT('Ctrl Pts',(-1.01778810567666,0.333333333333334,
-0.587620236790416)) ;
#48467=CARTESIAN_POINT('Ctrl Pts',(-0.678525403784438,0.291666666666667,
-1.17524047358083)) ;
#48468=CARTESIAN_POINT('Ctrl Pts',(0.,0.25,-1.17524047358083)) ;
#48469=CARTESIAN_POINT('Ctrl Pts',(0.678525403784437,0.208333333333334,
-1.17524047358083)) ;
#48470=CARTESIAN_POINT('Ctrl Pts',(1.01778810567666,0.166666666666667,-0.587620236790417)) ;
#48471=CARTESIAN_POINT('Ctrl Pts',(1.35705080756887,0.125,-8.30953963884777E-17)) ;
#48472=CARTESIAN_POINT('Ctrl Pts',(1.01778810567666,0.0833333333333337,
0.587620236790416)) ;
#48473=CARTESIAN_POINT('Ctrl Pts',(0.678525403784438,0.0416666666666671,
1.17524047358083)) ;
#48474=CARTESIAN_POINT('Ctrl Pts',(1.43925448419919E-16,2.16840434497101E-16,
1.17524047358083)) ;
#48475=CARTESIAN_POINT('Ctrl Pts',(-0.678525403784437,-0.0416666666666664,
1.17524047358083)) ;
#48476=CARTESIAN_POINT('Ctrl Pts',(-1.01778810567666,-0.0833333333333331,
0.587620236790417)) ;
#48477=CARTESIAN_POINT('Ctrl Pts',(-1.35705080756887,-0.125,2.49286189165433E-16)) ;
#48478=CARTESIAN_POINT('Ctrl Pts',(-1.01778810567666,-0.166666666666666,
-0.587620236790416)) ;
#48479=CARTESIAN_POINT('Ctrl Pts',(-0.678525403784438,-0.208333333333333,
-1.17524047358083)) ;
#48480=CARTESIAN_POINT('Ctrl Pts',(0.,-0.25,-1.17524047358083)) ;
#48481=CARTESIAN_POINT('Ctrl Pts',(0.678525403784437,-0.291666666666666,
-1.17524047358083)) ;
#48482=CARTESIAN_POINT('Ctrl Pts',(1.01778810567666,-0.333333333333333,
-0.587620236790417)) ;
#48483=CARTESIAN_POINT('Ctrl Pts',(1.35705080756887,-0.374999999999999,
-8.30953963884777E-17)) ;
#48484=CARTESIAN_POINT('Ctrl Pts',(1.01778810567666,-0.416666666666666,
0.587620236790416)) ;
#48485=CARTESIAN_POINT('Ctrl Pts',(0.678525403784438,-0.458333333333333,
1.17524047358083)) ;
#48486=CARTESIAN_POINT('Ctrl Pts',(1.43925448419919E-16,-0.5,1.17524047358083)) ;
#48487=CARTESIAN_POINT('Ctrl Pts',(-0.678525403784437,-0.541666666666666,
1.17524047358083)) ;
#48488=CARTESIAN_POINT('Ctrl Pts',(-1.01778810567666,-0.583333333333333,
0.587620236790417)) ;
#48489=CARTESIAN_POINT('Ctrl Pts',(-1.35705080756887,-0.625,2.49286189165433E-16)) ;
#48490=CARTESIAN_POINT('Ctrl Pts',(-1.01778810567666,-0.666666666666667,
-0.587620236790416)) ;
#48491=CARTESIAN_POINT('Ctrl Pts',(-0.678525403784438,-0.708333333333333,
-1.17524047358083)) ;
#48492=CARTESIAN_POINT('Ctrl Pts',(0.,-0.75,-1.17524047358083)) ;
#48493=CARTESIAN_POINT('Ctrl Pts',(0.678525403784437,-0.791666666666666,
-1.17524047358083)) ;
#48494=CARTESIAN_POINT('Ctrl Pts',(1.01778810567666,-0.833333333333333,
-0.587620236790417)) ;
#48495=CARTESIAN_POINT('Ctrl Pts',(1.35705080756887,-0.875,-8.30953963884777E-17)) ;
#48496=CARTESIAN_POINT('Ctrl Pts',(1.01778810567666,-0.916666666666666,
0.587620236790416)) ;
#48497=CARTESIAN_POINT('Ctrl Pts',(0.678525403784438,-0.958333333333333,
1.17524047358083)) ;
#48498=CARTESIAN_POINT('Ctrl Pts',(1.43925448419919E-16,-1.,1.17524047358083)) ;
#48499=CARTESIAN_POINT('Ctrl Pts',(-0.678525403784437,-1.04166666666667,
1.17524047358083)) ;
#48500=CARTESIAN_POINT('Ctrl Pts',(-1.01778810567666,-1.08333333333333,
0.587620236790417)) ;
#48501=CARTESIAN_POINT('Ctrl Pts',(-1.35705080756887,-1.125,2.49286189165433E-16)) ;
#48502=CARTESIAN_POINT('Ctrl Pts',(-1.01778810567666,-1.16666666666667,
-0.587620236790416)) ;
#48503=CARTESIAN_POINT('Ctrl Pts',(-0.678525403784438,-1.20833333333333,
-1.17524047358083)) ;
#48504=CARTESIAN_POINT('Ctrl Pts',(0.,-1.25,-1.17524047358083)) ;
#48505=CARTESIAN_POINT('Ctrl Pts',(0.678525403784437,-1.29166666666667,
-1.17524047358083)) ;
#48506=CARTESIAN_POINT('Ctrl Pts',(1.01778810567666,-1.33333333333333,-0.587620236790417)) ;
#48507=CARTESIAN_POINT('Ctrl Pts',(1.35705080756887,-1.375,-8.30953963884777E-17)) ;
#48508=CARTESIAN_POINT('Ctrl Pts',(1.01778810567666,-1.41666666666667,0.587620236790416)) ;
#48509=CARTESIAN_POINT('Ctrl Pts',(0.678525403784438,-1.45833333333333,
1.17524047358083)) ;
#48510=CARTESIAN_POINT('Ctrl Pts',(1.43925448419919E-16,-1.5,1.17524047358083)) ;
#48511=CARTESIAN_POINT('Ctrl Pts',(-0.678525403784437,-1.54166666666667,
1.17524047358083)) ;
#48512=CARTESIAN_POINT('Ctrl Pts',(-1.01778810567666,-1.58333333333333,
0.587620236790417)) ;
#48513=CARTESIAN_POINT('Ctrl Pts',(-1.35705080756887,-1.625,2.49286189165433E-16)) ;
#48514=CARTESIAN_POINT('Ctrl Pts',(-1.01778810567666,-1.66666666666667,
-0.587620236790416)) ;
#48515=CARTESIAN_POINT('Ctrl Pts',(-0.678525403784438,-1.70833333333333,
-1.17524047358083)) ;
#48516=CARTESIAN_POINT('Ctrl Pts',(0.,-1.75,-1.17524047358083)) ;
#48517=CARTESIAN_POINT('Origin',(-2.75,1.5,-1.58771324027147)) ;
#48518=CARTESIAN_POINT('',(2.75,1.5,0.)) ;
#48519=CARTESIAN_POINT('Origin',(0.,1.5,0.)) ;
#48520=CARTESIAN_POINT('',(1.375,1.5,-2.38156986040721)) ;
#48521=CARTESIAN_POINT('Origin',(0.,1.5,0.)) ;
#48522=CARTESIAN_POINT('',(-1.375,1.5,-2.38156986040721)) ;
#48523=CARTESIAN_POINT('Origin',(0.,1.5,0.)) ;
#48524=CARTESIAN_POINT('',(-2.75,1.5,3.7557864968429E-16)) ;
#48525=CARTESIAN_POINT('Origin',(0.,1.5,0.)) ;
#48526=CARTESIAN_POINT('Origin',(0.,1.5,0.)) ;
#48527=CARTESIAN_POINT('Origin',(9.59795089256626E-16,1.5,-3.17542648054295)) ;
#48528=CARTESIAN_POINT('',(7.2557076685516E-16,1.25437990693814,-3.17542648054295)) ;
#48529=CARTESIAN_POINT('',(9.59795089256626E-16,-1.25437990693814,-3.17542648054295)) ;
#48530=CARTESIAN_POINT('',(9.59795089256626E-16,1.5,-3.17542648054295)) ;
#48531=CARTESIAN_POINT('',(-1.375,-1.5,-2.38156986040721)) ;
#48532=CARTESIAN_POINT('Ctrl Pts',(5.29535621962484E-11,-1.25437990692049,
-3.17542648057352)) ;
#48533=CARTESIAN_POINT('Ctrl Pts',(-0.736860279164304,-1.5,-2.75000000001229)) ;
#48534=CARTESIAN_POINT('Ctrl Pts',(-1.375,-1.5,-2.38156986040721)) ;
#48535=CARTESIAN_POINT('',(-2.75,-1.25437990693838,-1.58771324027183)) ;
#48536=CARTESIAN_POINT('Ctrl Pts',(-1.375,-1.5,-2.38156986040721)) ;
#48537=CARTESIAN_POINT('Ctrl Pts',(-2.01313972081282,-1.5,-2.01313972081534)) ;
#48538=CARTESIAN_POINT('Ctrl Pts',(-2.74999999999603,-1.25437990693946,
-1.58771324027377)) ;
#48539=CARTESIAN_POINT('',(-2.75,1.25437990693835,-1.5877132402718)) ;
#48540=CARTESIAN_POINT('',(-2.75,1.5,-1.58771324027147)) ;
#48541=CARTESIAN_POINT('Ctrl Pts',(-1.37500000000001,1.5,-2.38156986040721)) ;
#48542=CARTESIAN_POINT('Ctrl Pts',(-2.01313972083563,1.5,-2.01313972080217)) ;
#48543=CARTESIAN_POINT('Ctrl Pts',(-2.75000000005277,1.25437990692055,-1.58771324024101)) ;
#48544=CARTESIAN_POINT('Ctrl Pts',(-3.77979605086846E-12,1.2543799069394,
-3.17542648054076)) ;
#48545=CARTESIAN_POINT('Ctrl Pts',(-0.736860279187109,1.5,-2.74999999999913)) ;
#48546=CARTESIAN_POINT('Ctrl Pts',(-1.37500000000001,1.5,-2.38156986040721)) ;
#48547=CARTESIAN_POINT('Origin',(-2.75,1.5,-1.58771324027147)) ;
#48548=CARTESIAN_POINT('',(-2.75,-1.5,3.7557864968429E-16)) ;
#48549=CARTESIAN_POINT('Ctrl Pts',(-2.75,-1.25437990692041,-1.58771324033287)) ;
#48550=CARTESIAN_POINT('Ctrl Pts',(-2.75,-1.5,-0.736860279210268)) ;
#48551=CARTESIAN_POINT('Ctrl Pts',(-2.75,-1.5,-4.52014535047054E-15)) ;
#48552=CARTESIAN_POINT('',(-2.75,-1.25437990693814,1.58771324027147)) ;
#48553=CARTESIAN_POINT('Ctrl Pts',(-2.75,-1.5,-4.52014535047054E-15)) ;
#48554=CARTESIAN_POINT('Ctrl Pts',(-2.75,-1.5,0.73686027918383)) ;
#48555=CARTESIAN_POINT('Ctrl Pts',(-2.75,-1.2543799069394,1.5877132402671)) ;
#48556=CARTESIAN_POINT('',(-2.75,1.25437990693814,1.58771324027147)) ;
#48557=CARTESIAN_POINT('',(-2.75,1.5,1.58771324027147)) ;
#48558=CARTESIAN_POINT('Ctrl Pts',(-2.75,1.5,5.10972952661887E-15)) ;
#48559=CARTESIAN_POINT('Ctrl Pts',(-2.75,1.5,0.736860279210163)) ;
#48560=CARTESIAN_POINT('Ctrl Pts',(-2.75,1.25437990692049,1.58771324033261)) ;
#48561=CARTESIAN_POINT('Ctrl Pts',(-2.75,1.25437990693933,-1.58771324026735)) ;
#48562=CARTESIAN_POINT('Ctrl Pts',(-2.75,1.5,-0.73686027918393)) ;
#48563=CARTESIAN_POINT('Ctrl Pts',(-2.75,1.5,5.10972952661887E-15)) ;
#48564=CARTESIAN_POINT('Origin',(-2.75,1.5,1.58771324027147)) ;
#48565=CARTESIAN_POINT('Ctrl Pts',(-2.75000000005296,-1.25437990692049,
1.58771324024089)) ;
#48566=CARTESIAN_POINT('Ctrl Pts',(-2.0131397208357,-1.5,2.01313972080212)) ;
#48567=CARTESIAN_POINT('Ctrl Pts',(-1.375,-1.5,2.3815698604072)) ;
#48568=CARTESIAN_POINT('',(-1.61031639274793E-15,1.5,3.17542648054294)) ;
#48569=CARTESIAN_POINT('Ctrl Pts',(-2.74999999999622,1.2543799069394,1.58771324027365)) ;
#48570=CARTESIAN_POINT('Ctrl Pts',(-2.01313972081289,1.5,2.01313972081529)) ;
#48571=CARTESIAN_POINT('Ctrl Pts',(-1.375,1.5,2.38156986040721)) ;
#48572=CARTESIAN_POINT('Origin',(-1.61031639274793E-15,1.5,3.17542648054294)) ;
#48573=CARTESIAN_POINT('',(2.75,-1.25437990693814,1.58771324027147)) ;
#48574=CARTESIAN_POINT('Ctrl Pts',(1.375,-1.5,2.3815698604072)) ;
#48575=CARTESIAN_POINT('Ctrl Pts',(2.01313972081289,-1.5,2.01313972081528)) ;
#48576=CARTESIAN_POINT('Ctrl Pts',(2.74999999999622,-1.2543799069394,1.58771324027365)) ;
#48577=CARTESIAN_POINT('',(2.75,1.25437990693814,1.58771324027147)) ;
#48578=CARTESIAN_POINT('',(2.75,1.5,1.58771324027147)) ;
#48579=CARTESIAN_POINT('Ctrl Pts',(1.375,1.5,2.3815698604072)) ;
#48580=CARTESIAN_POINT('Ctrl Pts',(2.0131397208357,1.5,2.01313972080212)) ;
#48581=CARTESIAN_POINT('Ctrl Pts',(2.75000000005295,1.25437990692049,1.58771324024089)) ;
#48582=CARTESIAN_POINT('Origin',(2.75,1.5,1.58771324027147)) ;
#48583=CARTESIAN_POINT('',(2.75,-1.5,0.)) ;
#48584=CARTESIAN_POINT('Ctrl Pts',(2.75,-1.25437990692049,1.58771324033261)) ;
#48585=CARTESIAN_POINT('Ctrl Pts',(2.75,-1.5,0.73686027921016)) ;
#48586=CARTESIAN_POINT('Ctrl Pts',(2.75,-1.5,7.86112234864441E-16)) ;
#48587=CARTESIAN_POINT('',(2.75,-1.25437990693814,-1.58771324027148)) ;
#48588=CARTESIAN_POINT('Ctrl Pts',(2.75,-1.5,7.86112234864441E-16)) ;
#48589=CARTESIAN_POINT('Ctrl Pts',(2.75,-1.5,-0.736860279183837)) ;
#48590=CARTESIAN_POINT('Ctrl Pts',(2.75,-1.2543799069394,-1.58771324026712)) ;
#48591=CARTESIAN_POINT('',(2.75,1.25437990693814,-1.58771324027148)) ;
#48592=CARTESIAN_POINT('',(2.75,1.5,-1.58771324027148)) ;
#48593=CARTESIAN_POINT('Ctrl Pts',(2.75,1.5,2.35833670459332E-15)) ;
#48594=CARTESIAN_POINT('Ctrl Pts',(2.75,1.5,-0.736860279210164)) ;
#48595=CARTESIAN_POINT('Ctrl Pts',(2.75,1.25437990692049,-1.58771324033262)) ;
#48596=CARTESIAN_POINT('Ctrl Pts',(2.75,1.2543799069394,1.58771324026711)) ;
#48597=CARTESIAN_POINT('Ctrl Pts',(2.75,1.5,0.736860279183835)) ;
#48598=CARTESIAN_POINT('Ctrl Pts',(2.75,1.5,2.35833670459332E-15)) ;
#48599=CARTESIAN_POINT('Origin',(2.75,1.5,-1.58771324027148)) ;
#48600=CARTESIAN_POINT('',(1.375,-1.5,-2.38156986040721)) ;
#48601=CARTESIAN_POINT('Ctrl Pts',(2.75000000005296,-1.25437990692049,-1.5877132402409)) ;
#48602=CARTESIAN_POINT('Ctrl Pts',(2.0131397208357,-1.5,-2.01313972080213)) ;
#48603=CARTESIAN_POINT('Ctrl Pts',(1.375,-1.5,-2.38156986040721)) ;
#48604=CARTESIAN_POINT('Ctrl Pts',(1.375,-1.5,-2.38156986040721)) ;
#48605=CARTESIAN_POINT('Ctrl Pts',(0.736860279187108,-1.5,-2.74999999999913)) ;
#48606=CARTESIAN_POINT('Ctrl Pts',(3.78043123953934E-12,-1.2543799069394,
-3.17542648054077)) ;
#48607=CARTESIAN_POINT('Ctrl Pts',(1.375,1.5,-2.38156986040721)) ;
#48608=CARTESIAN_POINT('Ctrl Pts',(0.736860279164306,1.5,-2.75000000001229)) ;
#48609=CARTESIAN_POINT('Ctrl Pts',(-5.29512331711219E-11,1.25437990692049,
-3.17542648057352)) ;
#48610=CARTESIAN_POINT('Ctrl Pts',(2.74999999999623,1.2543799069394,-1.58771324027366)) ;
#48611=CARTESIAN_POINT('Ctrl Pts',(2.0131397208129,1.5,-2.01313972081529)) ;
#48612=CARTESIAN_POINT('Ctrl Pts',(1.375,1.5,-2.38156986040721)) ;
#48613=CARTESIAN_POINT('Origin',(-2.75,-1.5,-1.58771324027147)) ;
#48614=CARTESIAN_POINT('Origin',(0.,-1.5,0.)) ;
#48615=CARTESIAN_POINT('Origin',(0.,-1.5,0.)) ;
#48616=CARTESIAN_POINT('Origin',(0.,-1.5,0.)) ;
#48617=CARTESIAN_POINT('Origin',(0.,-1.5,0.)) ;
#48618=CARTESIAN_POINT('Origin',(0.,-1.5,0.)) ;
#48619=CARTESIAN_POINT('Origin',(0.,1.5,0.)) ;
#48620=CARTESIAN_POINT('Origin',(0.,1.5,0.)) ;
#48621=CARTESIAN_POINT('Origin',(0.,1.5,0.)) ;
#48622=CARTESIAN_POINT('Origin',(0.,1.5,0.)) ;
#48623=CARTESIAN_POINT('Origin',(0.,1.5,0.)) ;
#48624=CARTESIAN_POINT('Origin',(0.,-1.5,0.)) ;
#48625=CARTESIAN_POINT('Origin',(0.,-1.5,0.)) ;
#48626=CARTESIAN_POINT('Origin',(0.,-1.5,0.)) ;
#48627=CARTESIAN_POINT('Origin',(0.,-1.5,0.)) ;
#48628=CARTESIAN_POINT('Origin',(0.,-1.5,0.)) ;
#86284=UNCERTAINTY_MEASURE_WITH_UNIT(LENGTH_MEASURE(0.01),#86331,
'DISTANCE_ACCURACY_VALUE',
'Maximum model space distance between geometric entities at asserted c
onnectivities') ;
#86304=UNCERTAINTY_MEASURE_WITH_UNIT(LENGTH_MEASURE(0.01),#86331,
'DISTANCE_ACCURACY_VALUE',
'Maximum model space distance between geometric entities at asserted c
onnectivities') ;
#86310=(
GEOMETRIC_REPRESENTATION_CONTEXT(3)
GLOBAL_UNCERTAINTY_ASSIGNED_CONTEXT((#86284))
GLOBAL_UNIT_ASSIGNED_CONTEXT((#86331,#86333,#86334))
REPRESENTATION_CONTEXT('','3D')
) ;
#86330=(
GEOMETRIC_REPRESENTATION_CONTEXT(3)
GLOBAL_UNCERTAINTY_ASSIGNED_CONTEXT((#86304))
GLOBAL_UNIT_ASSIGNED_CONTEXT((#86331,#86333,#86334))
REPRESENTATION_CONTEXT('','3D')
) ;
#86331=(
LENGTH_UNIT()
NAMED_UNIT(*)
SI_UNIT(.MILLI.,.METRE.)
) ;
#86333=(
NAMED_UNIT(*)
PLANE_ANGLE_UNIT()
SI_UNIT($,.RADIAN.)
) ;
#86334=(
NAMED_UNIT(*)
SI_UNIT($,.STERADIAN.)
SOLID_ANGLE_UNIT()
) ;
#86340=SHAPE_DEFINITION_REPRESENTATION(#86365,#86456) ;
#86365=PRODUCT_DEFINITION_SHAPE('',$,#86482) ;
#86456=SHAPE_REPRESENTATION('',(#33062),#86310) ;
#86476=PRODUCT_DEFINITION_CONTEXT('part definition',#86553,'design') ;
#86482=PRODUCT_DEFINITION('Hex_Nut','Hex_Nut',#86507,#86476) ;
#86507=PRODUCT_DEFINITION_FORMATION('',$,#86560) ;
#86553=APPLICATION_CONTEXT(
'Core Data for Automotive Mechanical Design Process') ;
#86554=PRODUCT_CONTEXT('part definition',#86553,'mechanical') ;
#86560=PRODUCT('Hex_Nut','Hex_Nut',$,(#86554)) ;
#86582=PRESENTATION_STYLE_ASSIGNMENT((#86587)) ;
#86587=SURFACE_STYLE_USAGE(.BOTH.,#86592) ;
#86592=SURFACE_SIDE_STYLE('',(#86597)) ;
#86597=SURFACE_STYLE_FILL_AREA(#86602) ;
#86602=FILL_AREA_STYLE('Opaque(203,203,203)',(#86607)) ;
#86607=FILL_AREA_STYLE_COLOUR('Opaque(203,203,203)',#86612) ;
#86612=COLOUR_RGB('Opaque(203,203,203)', 0.66274510, 0.83137255, 0.94901961) ;
ENDSEC;
END-ISO-10303-21;
